ISO-10303-21;
HEADER;
FILE_DESCRIPTION (('STEP AP214'),
    '1' );
FILE_NAME ('hex flange nut gradea_iso_ISO - 4161 - M8 - N.step',
    '2026-10-27T17:01:19',
    ( '' ),
    ( '' ),
    'SwSTEP 2.0',
    'SolidWorks 2026',
    '' );
FILE_SCHEMA (( 'AUTOMOTIVE_DESIGN' ));
ENDSEC;

DATA;
#6=CARTESIAN_POINT ( 'NONE',  ( 1.058054217398695762, -6.894685612232789751, -0.3576316571898509600 ) ) ;
#18=EDGE_LOOP ( 'NONE', ( #9492, #7040, #7243, #2975 ) ) ;
#32=CARTESIAN_POINT ( 'NONE',  ( 0.000000000000000000, 0.000000000000000000, -25.03750572909317285 ) ) ;
#57=CARTESIAN_POINT ( 'NONE',  ( -6.500000000000000000, 3.752776749732564809, -6.064240316920399110 ) ) ;
#61=DIRECTION ( 'NONE',  ( 0.000000000000000000, 0.000000000000000000, 1.000000000000000000 ) ) ;
#86=ORIENTED_EDGE ( 'NONE', *, *, #13517, .T. ) ;
#89=CARTESIAN_POINT ( 'NONE',  ( 0.000000000000000000, 0.000000000000000000, -7.381345277524544279 ) ) ;
#151=VERTEX_POINT ( 'NONE', #13018 ) ;
#177=MECHANICAL_DESIGN_GEOMETRIC_PRESENTATION_REPRESENTATION('',(#1004),#8687);
#184=CARTESIAN_POINT ( 'NONE',  ( -6.826425371444817536, 2.641426549045769345, -6.344843397090116355 ) ) ;
#204=CARTESIAN_POINT ( 'NONE',  ( 6.269955739554010421, 4.268932597852939104, -6.443844059477442876 ) ) ;
#208=CIRCLE ( 'NONE', #11778, 8.542937654374687995 ) ;
#228=CARTESIAN_POINT ( 'NONE',  ( 2.263183130831067924, -6.566419505188284766, -6.208110906918261840 ) ) ;
#260=( BOUNDED_SURFACE ( )  B_SPLINE_SURFACE ( 3, 2, ( 
 ( #2546, #4855, #7134 ),
 ( #13843, #1521, #11762 ),
 ( #3742, #1668, #2637 ),
 ( #552, #8754, #12960 ),
 ( #1882, #8671, #14357 ),
 ( #14286, #6532, #7425 ),
 ( #11025, #772, #8601 ),
 ( #4037, #14440, #13175 ) ),
 .UNSPECIFIED., .F., .F., .F. ) 
 B_SPLINE_SURFACE_WITH_KNOTS ( ( 4, 2, 2, 4 ),
 ( 3, 3 ),
 ( 0.03170918191602133812, 0.03570420671717101924, 0.03770171911774586326, 0.03969923151832070729 ),
 ( 0.000000000000000000, 1.000000000000000000 ),
 .UNSPECIFIED. ) 
 GEOMETRIC_REPRESENTATION_ITEM ( )  RATIONAL_B_SPLINE_SURFACE ( (
 ( 1.000000000000000000, 0.8047781070930550840, 1.000000000000000000),
 ( 1.000000000000000000, 0.8123787894255611874, 1.000000000000000000),
 ( 1.000000000000000000, 0.8190667557154468481, 1.000000000000000000),
 ( 1.000000000000000000, 0.8191933945820784047, 1.000000000000000000),
 ( 1.000000000000000000, 0.8176087340369108114, 1.000000000000000000),
 ( 1.000000000000000000, 0.8122956952719621038, 1.000000000000000000),
 ( 1.000000000000000000, 0.8086308540103167575, 1.000000000000000000),
 ( 1.000000000000000000, 0.8047712493762134711, 1.000000000000000000) ) ) 
 REPRESENTATION_ITEM ( '' )  SURFACE ( )  );
#266=FACE_OUTER_BOUND ( 'NONE', #13109, .T. ) ;
#282=ADVANCED_FACE ( 'NONE', ( #6369 ), #14593, .F. ) ;
#315=ORIENTED_EDGE ( 'NONE', *, *, #8291, .F. ) ;
#317=FACE_OUTER_BOUND ( 'NONE', #9908, .T. ) ;
#340=ORIENTED_EDGE ( 'NONE', *, *, #7667, .F. ) ;
#358=VERTEX_POINT ( 'NONE', #9242 ) ;
#360=CARTESIAN_POINT ( 'NONE',  ( 6.815830331203684089, -0.6610623347507956771, -6.171384342982605631 ) ) ;
#364=ADVANCED_FACE ( 'NONE', ( #9021 ), #12395, .F. ) ;
#391=B_SPLINE_CURVE_WITH_KNOTS ( 'NONE', 3,
 ( #1032, #1097, #10197, #13582, #57 ),
 .UNSPECIFIED., .F., .F.,
 ( 4, 1, 4 ),
 ( 0.000000000000000000, 0.003752776749732567897, 0.007505553499465135794 ),
 .UNSPECIFIED. ) ;
#395=CONICAL_SURFACE ( 'NONE', #2539, 8.542937654374687995, 1.221730476396047926 ) ;
#438=CARTESIAN_POINT ( 'NONE',  ( -3.755786496842903988E-16, -7.505553499465146494, -6.064240316920404439 ) ) ;
#446=VECTOR ( 'NONE', #14480, 1000.000000000000000 ) ;
#448=DIRECTION ( 'NONE',  ( 0.000000000000000000, 0.000000000000000000, 1.000000000000000000 ) ) ;
#454=CARTESIAN_POINT ( 'NONE',  ( 4.555432764205793461, -5.242992371775935467, -6.208169345099792125 ) ) ;
#457=CARTESIAN_POINT ( 'NONE',  ( 3.999999999999999112, 0.000000000000000000, 3.469446951953614189E-15 ) ) ;
#462=B_SPLINE_CURVE_WITH_KNOTS ( 'NONE', 3,
 ( #3641, #5917, #4823, #1271, #11380, #5770 ),
 .UNSPECIFIED., .F., .F.,
 ( 4, 2, 4 ),
 ( 0.003841072314098351557, 0.005765657563962180328, 0.007690242813826009098 ),
 .UNSPECIFIED. ) ;
#486=CARTESIAN_POINT ( 'NONE',  ( 2.688402820137697713, 5.953403407568487182, -0.01956314070068190455 ) ) ;
#488=VERTEX_POINT ( 'NONE', #6052 ) ;
#508=COLOUR_RGB ( '',1.000000000000000000, 0.9490196078431372140, 0.9098039215686274384 ) ;
#510=DIRECTION ( 'NONE',  ( -0.5000000000000006661, 0.8660254037844382635, 0.000000000000000000 ) ) ;
#537=CARTESIAN_POINT ( 'NONE',  ( 0.000000000000000000, 0.000000000000000000, -7.974599999999998801 ) ) ;
#538=B_SPLINE_CURVE_WITH_KNOTS ( 'NONE', 3,
 ( #12622, #10265, #10551, #11651, #1547, #4663 ),
 .UNSPECIFIED., .F., .F.,
 ( 4, 2, 4 ),
 ( -4.604908129293502741E-06, 0.0003318387708540405283, 0.0006682824498373745670 ),
 .UNSPECIFIED. ) ;
#546=DIRECTION ( 'NONE',  ( -1.000000000000000000, 0.000000000000000000, 0.000000000000000000 ) ) ;
#548=CARTESIAN_POINT ( 'NONE',  ( 5.416666666666667851, 4.378239541354659536, -5.848636054922034866 ) ) ;
#552=CARTESIAN_POINT ( 'NONE',  ( 6.500000000000000000, 0.6659426636835951152, -5.719325464431898709 ) ) ;
#553=PLANE ( 'NONE',  #13381 ) ;
#575=CARTESIAN_POINT ( 'NONE',  ( 3.250000000000003109, -5.629165124598849879, 0.000000000000000000 ) ) ;
#603=CARTESIAN_POINT ( 'NONE',  ( 3.250000000000004441, 5.629165124598849879, 0.000000000000000000 ) ) ;
#615=DIRECTION ( 'NONE',  ( 0.000000000000000000, 0.000000000000000000, 1.000000000000000000 ) ) ;
#622=EDGE_CURVE ( 'NONE', #14203, #358, #1002, .T. ) ;
#633=DIRECTION ( 'NONE',  ( 1.000000000000000000, 0.000000000000000000, 0.000000000000000000 ) ) ;
#655=PRODUCT_CONTEXT ( 'NONE', #3018, 'mechanical' ) ;
#664=EDGE_CURVE ( 'NONE', #7485, #11091, #11934, .T. ) ;
#692=FACE_OUTER_BOUND ( 'NONE', #2128, .T. ) ;
#772=CARTESIAN_POINT ( 'NONE',  ( 6.500000000000296652, 3.350125858420170299, -6.343571411523281967 ) ) ;
#782=ADVANCED_FACE ( 'NONE', ( #10186 ), #9072, .T. ) ;
#785=ADVANCED_FACE ( 'NONE', ( #11425 ), #10715, .T. ) ;
#797=ORIENTED_EDGE ( 'NONE', *, *, #3556, .T. ) ;
#798=CARTESIAN_POINT ( 'NONE',  ( 3.783380760145018981E-16, -7.895640089090872671, -6.564402953523720718 ) ) ;
#815=CARTESIAN_POINT ( 'NONE',  ( -2.055025722542106692, 6.319083845363845597, -5.720331885005371930 ) ) ;
#817=CARTESIAN_POINT ( 'NONE',  ( -6.500000000000000888, 1.416734669062281959, -5.722373386996368438 ) ) ;
#821=CARTESIAN_POINT ( 'NONE',  ( -1.127757440534757460, -7.231345287187099125, -6.344532336093708480 ) ) ;
#823=ORIENTED_EDGE ( 'NONE', *, *, #6899, .F. ) ;
#833=ADVANCED_FACE ( 'NONE', ( #1254 ), #10098, .F. ) ;
#835=DIRECTION ( 'NONE',  ( -1.000000000000000000, 0.000000000000000000, 0.000000000000000000 ) ) ;
#859=EDGE_CURVE ( 'NONE', #3582, #13126, #12261, .T. ) ;
#875=AXIS2_PLACEMENT_3D ( 'NONE', #6179, #8309, #10678 ) ;
#876=ORIENTED_EDGE ( 'NONE', *, *, #4951, .F. ) ;
#893=ORIENTED_EDGE ( 'NONE', *, *, #8420, .F. ) ;
#926=AXIS2_PLACEMENT_3D ( 'NONE', #1440, #4912, #12807 ) ;
#931=VERTEX_POINT ( 'NONE', #6035 ) ;
#951=VECTOR ( 'NONE', #5253, 1000.000000000000000 ) ;
#975=FILL_AREA_STYLE_COLOUR ( '', #508 ) ;
#1002=B_SPLINE_CURVE_WITH_KNOTS ( 'NONE', 3,
 ( #6499, #8853, #13073, #14469, #9816, #1834 ),
 .UNSPECIFIED., .F., .F.,
 ( 4, 2, 4 ),
 ( 0.000000000000000000, 0.001990940508721414457, 0.003981881017442828914 ),
 .UNSPECIFIED. ) ;
#1004=STYLED_ITEM('',(#14681),#12340);
#1026=B_SPLINE_CURVE_WITH_KNOTS ( 'NONE', 3,
 ( #1997, #8723, #14195, #3932, #1850 ),
 .UNSPECIFIED., .F., .F.,
 ( 4, 1, 4 ),
 ( 0.000000000000000000, 0.003752776749732569198, 0.007505553499465138396 ),
 .UNSPECIFIED. ) ;
#1032=CARTESIAN_POINT ( 'NONE',  ( -5.357619327558936585E-16, 7.505553499465137612, -6.064240316920400886 ) ) ;
#1049=CARTESIAN_POINT ( 'NONE',  ( 0.000000000000000000, 0.000000000000000000, -0.4201245229258211977 ) ) ;
#1050=ORIENTED_EDGE ( 'NONE', *, *, #3760, .T. ) ;
#1052=ORIENTED_EDGE ( 'NONE', *, *, #7592, .F. ) ;
#1065=EDGE_CURVE ( 'NONE', #11091, #2224, #12196, .T. ) ;
#1089=DIRECTION ( 'NONE',  ( -0.000000000000000000, -0.000000000000000000, 1.000000000000000000 ) ) ;
#1094=DIRECTION ( 'NONE',  ( 0.000000000000000000, 0.000000000000000000, 1.000000000000000000 ) ) ;
#1097=CARTESIAN_POINT ( 'NONE',  ( -1.083333333333333259, 6.880090707843040221, -5.848636054922037530 ) ) ;
#1101=CARTESIAN_POINT ( 'NONE',  ( -5.727634848077285845, 4.575561887448583498, -6.326622577870772979 ) ) ;
#1120=VERTEX_POINT ( 'NONE', #9039 ) ;
#1125=DIRECTION ( 'NONE',  ( 0.000000000000000000, 0.000000000000000000, 1.000000000000000000 ) ) ;
#1136=ORIENTED_EDGE ( 'NONE', *, *, #3332, .T. ) ;
#1154=ORIENTED_EDGE ( 'NONE', *, *, #7723, .F. ) ;
#1190=( NAMED_UNIT ( * ) SI_UNIT ( $, .STERADIAN. ) SOLID_ANGLE_UNIT ( ) );
#1192=CYLINDRICAL_SURFACE ( 'NONE', #2355, 3.399999999999999911 ) ;
#1234=CIRCLE ( 'NONE', #4306, 3.999999999999999112 ) ;
#1254=FACE_OUTER_BOUND ( 'NONE', #6553, .T. ) ;
#1271=CARTESIAN_POINT ( 'NONE',  ( -1.058054217398698871, 6.894685612232779981, -0.3576316571898437990 ) ) ;
#1296=B_SPLINE_CURVE_WITH_KNOTS ( 'NONE', 3,
 ( #6642, #11136, #2043, #3236, #14607, #4499 ),
 .UNSPECIFIED., .F., .F.,
 ( 4, 2, 4 ),
 ( 0.005511122051665403969, 0.007432374760074392586, 0.009353627468483380336 ),
 .UNSPECIFIED. ) ;
#1304=B_SPLINE_CURVE_WITH_KNOTS ( 'NONE', 3,
 ( #603, #1730, #12725, #2624, #5067, #6232 ),
 .UNSPECIFIED., .F., .F.,
 ( 4, 2, 4 ),
 ( 0.003841072314098362400, 0.005765657563962184665, 0.007690242813826007363 ),
 .UNSPECIFIED. ) ;
#1309=CARTESIAN_POINT ( 'NONE',  ( 6.725979247667765115, -3.622307570260320020, -6.470294263593358686 ) ) ;
#1337=CARTESIAN_POINT ( 'NONE',  ( 6.500000000000000000, -3.752776749732574135, -6.064240316920400886 ) ) ;
#1341=ORIENTED_EDGE ( 'NONE', *, *, #6974, .F. ) ;
#1345=DIRECTION ( 'NONE',  ( 1.000000000000000000, 0.000000000000000000, 0.000000000000000000 ) ) ;
#1364=VERTEX_POINT ( 'NONE', #457 ) ;
#1372=CARTESIAN_POINT ( 'NONE',  ( 0.000000000000000000, 0.000000000000000000, -6.800000000000000711 ) ) ;
#1382=CARTESIAN_POINT ( 'NONE',  ( -1.604619215278546562E-14, -7.505553499465138501, -0.8000000000000003775 ) ) ;
#1383=AXIS2_PLACEMENT_3D ( 'NONE', #10321, #13800, #5975 ) ;
#1391=CARTESIAN_POINT ( 'NONE',  ( 0.2259792476677697226, -7.636022678937403718, -6.470294263593365791 ) ) ;
#1397=( BOUNDED_SURFACE ( )  B_SPLINE_SURFACE ( 3, 2, ( 
 ( #9618, #13347, #4359 ),
 ( #6710, #2911, #7408 ),
 ( #9965, #11061, #9701 ),
 ( #11894, #4423, #8851 ),
 ( #7747, #14201, #4014 ),
 ( #8921, #8510, #12938 ) ),
 .UNSPECIFIED., .F., .F., .F. ) 
 B_SPLINE_SURFACE_WITH_KNOTS ( ( 4, 2, 4 ),
 ( 3, 3 ),
 ( 0.003190620565844220352, 0.007281897438794486706, 0.01137317431174475306 ),
 ( 0.000000000000000000, 1.000000000000000000 ),
 .UNSPECIFIED. ) 
 GEOMETRIC_REPRESENTATION_ITEM ( )  RATIONAL_B_SPLINE_SURFACE ( (
 ( 1.000000000000000000, 0.8047731410850402778, 1.000000000000000000),
 ( 1.000000000000000000, 0.8125552299142427826, 1.000000000000000000),
 ( 1.000000000000000000, 0.8191520442908248878, 1.000000000000000000),
 ( 1.000000000000000000, 0.8191520442871482732, 1.000000000000000000),
 ( 1.000000000000000000, 0.8125552299170040182, 1.000000000000000000),
 ( 1.000000000000000000, 0.8047731410850399447, 1.000000000000000000) ) ) 
 REPRESENTATION_ITEM ( '' )  SURFACE ( )  );
#1405=AXIS2_PLACEMENT_3D ( 'NONE', #5448, #7508, #10976 ) ;
#1440=CARTESIAN_POINT ( 'NONE',  ( 0.000000000000000000, 0.000000000000000000, 0.000000000000000000 ) ) ;
#1464=CARTESIAN_POINT ( 'NONE',  ( 6.781345014477444089, -3.590342129888862921, -6.122077150241852728 ) ) ;
#1468=AXIS2_PLACEMENT_3D ( 'NONE', #8105, #13796, #9136 ) ;
#1483=DIRECTION ( 'NONE',  ( 0.000000000000000000, 0.000000000000000000, 1.000000000000000000 ) ) ;
#1490=DIRECTION ( 'NONE',  ( 1.000000000000000000, 0.000000000000000000, 0.000000000000000000 ) ) ;
#1494=ORIENTED_EDGE ( 'NONE', *, *, #8612, .F. ) ;
#1500=ORIENTED_EDGE ( 'NONE', *, *, #7365, .T. ) ;
#1519=ORIENTED_EDGE ( 'NONE', *, *, #9574, .F. ) ;
#1521=CARTESIAN_POINT ( 'NONE',  ( 6.500000000000576428, -2.723981882618385697, -6.224051986860747121 ) ) ;
#1522=CARTESIAN_POINT ( 'NONE',  ( -6.837824896291514243, 3.947820044545427454, -6.564402953523716278 ) ) ;
#1547=CARTESIAN_POINT ( 'NONE',  ( -6.500000000000000888, -3.752776749732573247, -6.177802698399960768 ) ) ;
#1555=FACE_OUTER_BOUND ( 'NONE', #14485, .T. ) ;
#1557=ORIENTED_EDGE ( 'NONE', *, *, #3933, .T. ) ;
#1586=EDGE_CURVE ( 'NONE', #4487, #4582, #462, .T. ) ;
#1587=CARTESIAN_POINT ( 'NONE',  ( -6.500000000000000000, 3.752776749732564809, -8.000000000000000000 ) ) ;
#1593=EDGE_LOOP ( 'NONE', ( #7270, #9100, #14362 ) ) ;
#1629=DIRECTION ( 'NONE',  ( 1.000000000000000000, 0.000000000000000000, 0.000000000000000000 ) ) ;
#1631=ORIENTED_EDGE ( 'NONE', *, *, #2654, .T. ) ;
#1649=LINE ( 'NONE', #13910, #10791 ) ;
#1650=( NAMED_UNIT ( * ) SI_UNIT ( $, .STERADIAN. ) SOLID_ANGLE_UNIT ( ) );
#1655=ORIENTED_EDGE ( 'NONE', *, *, #11956, .T. ) ;
#1668=CARTESIAN_POINT ( 'NONE',  ( 6.499999999999398703, -1.392325603688425284, -6.058577540042510812 ) ) ;
#1676=CARTESIAN_POINT ( 'NONE',  ( 1.049032378833991030, 6.899894373156697291, -0.3607371497494544221 ) ) ;
#1701=CARTESIAN_POINT ( 'NONE',  ( 3.811597179862312057, -5.304926841629219680, -0.01956314070068839589 ) ) ;
#1722=ORIENTED_EDGE ( 'NONE', *, *, #3760, .F. ) ;
#1730=CARTESIAN_POINT ( 'NONE',  ( 3.809068165403724393, 5.306386968807659699, 9.757819552369535962E-16 ) ) ;
#1731=ORIENTED_EDGE ( 'NONE', *, *, #11221, .F. ) ;
#1735=CARTESIAN_POINT ( 'NONE',  ( 0.000000000000000000, 0.000000000000000000, 3.469446951953614189E-15 ) ) ;
#1759=CARTESIAN_POINT ( 'NONE',  ( 6.500000000000005329, -3.752776749732571027, -6.177805531629060987 ) ) ;
#1769=EDGE_CURVE ( 'NONE', #12254, #9582, #9397, .T. ) ;
#1772=SHAPE_DEFINITION_REPRESENTATION ( #11462, #1780 ) ;
#1780=SHAPE_REPRESENTATION ( 'hex flange nut gradea_iso_ISO - 4161 - M8 - N', ( #9440 ), #13250 ) ;
#1817=CARTESIAN_POINT ( 'NONE',  ( -3.999999999999999112, 0.000000000000000000, -7.974599999999998801 ) ) ;
#1825=CARTESIAN_POINT ( 'NONE',  ( -6.500000000000000888, 0.6470732608156811727, -0.01945970098673090176 ) ) ;
#1834=CARTESIAN_POINT ( 'NONE',  ( -6.815830331203685866, -1.210827632163352847E-13, -6.171384342982610960 ) ) ;
#1840=AXIS2_PLACEMENT_3D ( 'NONE', #14104, #9680, #1490 ) ;
#1848=CARTESIAN_POINT ( 'NONE',  ( 4.000000000000000000, 0.000000000000000000, -8.000000000000000000 ) ) ;
#1850=CARTESIAN_POINT ( 'NONE',  ( -3.755786496842903988E-16, -7.505553499465146494, -6.064240316920404439 ) ) ;
#1882=CARTESIAN_POINT ( 'NONE',  ( 6.500000000000000888, 1.355443906731431669, -5.756734754743127347 ) ) ;
#1897=VERTEX_POINT ( 'NONE', #14472 ) ;
#1908=CARTESIAN_POINT ( 'NONE',  ( -6.500000000000000000, 2.536640449112271156, -0.3753468889000206032 ) ) ;
#1924=LINE ( 'NONE', #14397, #14128 ) ;
#1935=CARTESIAN_POINT ( 'NONE',  ( 0.5619217318086654478, 7.564468822943301696, -6.443866470201762731 ) ) ;
#1939=CARTESIAN_POINT ( 'NONE',  ( -6.826580258811596025, 2.695816818222440681, -6.331007506863580048 ) ) ;
#1945=ORIENTED_EDGE ( 'NONE', *, *, #14180, .T. ) ;
#1953=DIRECTION ( 'NONE',  ( 1.000000000000000000, 0.000000000000000000, 0.000000000000000000 ) ) ;
#1974=DIRECTION ( 'NONE',  ( -1.000000000000000000, 0.000000000000000000, 0.000000000000000000 ) ) ;
#1997=CARTESIAN_POINT ( 'NONE',  ( -6.500000000000000000, -3.752776749732572803, -6.064240316920399998 ) ) ;
#1998=CARTESIAN_POINT ( 'NONE',  ( 6.500000000000001776, -5.204170427930421283E-15, -5.592027715088708995 ) ) ;
#2005=ADVANCED_FACE ( 'NONE', ( #7962 ), #6104, .F. ) ;
#2040=CARTESIAN_POINT ( 'NONE',  ( 2.075968632162763061, -6.306992450856140131, -6.056431503344847478 ) ) ;
#2043=CARTESIAN_POINT ( 'NONE',  ( 6.500000000000000888, -2.534234941938116936, -0.3584823952106179212 ) ) ;
#2062=CARTESIAN_POINT ( 'NONE',  ( -4.444974277457898637, 4.939246403833854160, -5.720331885005371930 ) ) ;
#2066=CARTESIAN_POINT ( 'NONE',  ( -6.500000000000000888, -2.727365451017189635, -5.874157743775032969 ) ) ;
#2085=CARTESIAN_POINT ( 'NONE',  ( 0.5219667817988800085, -7.204195837485521281, -0.5602453477493418710 ) ) ;
#2087=CIRCLE ( 'NONE', #13176, 8.331345277524542681 ) ;
#2089=CARTESIAN_POINT ( 'NONE',  ( 3.399999999999999911, 0.000000000000000000, -8.000000000000000000 ) ) ;
#2113=VERTEX_POINT ( 'NONE', #11428 ) ;
#2128=EDGE_LOOP ( 'NONE', ( #10320, #2717, #14381, #1494, #3706, #8597, #10276 ) ) ;
#2134=CIRCLE ( 'NONE', #13699, 3.399999999999999911 ) ;
#2135=CARTESIAN_POINT ( 'NONE',  ( 6.500000000000000000, 3.752776749732563921, -6.064240316920399110 ) ) ;
#2139=CARTESIAN_POINT ( 'NONE',  ( 0.000000000000000000, 0.000000000000000000, -8.000000000000000000 ) ) ;
#2144=CARTESIAN_POINT ( 'NONE',  ( -6.878751942472531411, 3.924677726130923361, -6.573129608219089981 ) ) ;
#2182=ORIENTED_EDGE ( 'NONE', *, *, #4749, .F. ) ;
#2187=DIRECTION ( 'NONE',  ( -1.000000000000000000, 0.000000000000000000, 0.000000000000000000 ) ) ;
#2224=VERTEX_POINT ( 'NONE', #7599 ) ;
#2232=EDGE_CURVE ( 'NONE', #2113, #4509, #4937, .T. ) ;
#2252=CARTESIAN_POINT ( 'NONE',  ( -1.049032378834002577, -6.899894373156699068, -0.3607371497494579748 ) ) ;
#2269=CARTESIAN_POINT ( 'NONE',  ( -4.444974277458378253, -4.939246403833585042, -5.720331885005373707 ) ) ;
#2273=CARTESIAN_POINT ( 'NONE',  ( 6.663127973346361976, 3.846958729056444426, -6.460793508093577664 ) ) ;
#2306=B_SPLINE_CURVE_WITH_KNOTS ( 'NONE', 3,
 ( #11439, #10765, #13130, #14309, #9749, #798 ),
 .UNSPECIFIED., .F., .F.,
 ( 4, 2, 4 ),
 ( 8.673617379884035472E-19, 0.0003352299596267603100, 0.0006704599192535197526 ),
 .UNSPECIFIED. ) ;
#2355=AXIS2_PLACEMENT_3D ( 'NONE', #12339, #8060, #4378 ) ;
#2357=PLANE ( 'NONE',  #6612 ) ;
#2363=EDGE_CURVE ( 'NONE', #1120, #13126, #13051, .T. ) ;
#2389=CARTESIAN_POINT ( 'NONE',  ( 3.250000000000003109, -5.629165124598849879, 0.000000000000000000 ) ) ;
#2399=ORIENTED_EDGE ( 'NONE', *, *, #3834, .T. ) ;
#2405=DIRECTION ( 'NONE',  ( -0.000000000000000000, -0.000000000000000000, 1.000000000000000000 ) ) ;
#2455=CARTESIAN_POINT ( 'NONE',  ( -3.250000000000004441, 5.629165124598849879, 0.000000000000000000 ) ) ;
#2457=ORIENTED_EDGE ( 'NONE', *, *, #8828, .F. ) ;
#2470=DIRECTION ( 'NONE',  ( 1.000000000000000000, 0.000000000000000000, 0.000000000000000000 ) ) ;
#2495=CARTESIAN_POINT ( 'NONE',  ( -5.619193549420757883, -4.261310591078458110, -5.875704392893551287 ) ) ;
#2539=AXIS2_PLACEMENT_3D ( 'NONE', #4039, #4329, #835 ) ;
#2541=EDGE_CURVE ( 'NONE', #14499, #13769, #11958, .T. ) ;
#2546=CARTESIAN_POINT ( 'NONE',  ( 6.500000000000000888, -4.076778466486154606, -6.121917890101376436 ) ) ;
#2580=CARTESIAN_POINT ( 'NONE',  ( -0.9108756637653833144, 6.979659189792688956, -6.219623095965475024 ) ) ;
#2586=AXIS2_PLACEMENT_3D ( 'NONE', #14163, #4057, #5307 ) ;
#2604=CARTESIAN_POINT ( 'NONE',  ( 6.818286579240217193, -1.325012739682874141, -6.208253321455268647 ) ) ;
#2624=CARTESIAN_POINT ( 'NONE',  ( 5.441945782601302462, 4.363644636964922441, -0.3576316571898402463 ) ) ;
#2626=ORIENTED_EDGE ( 'NONE', *, *, #4337, .F. ) ;
#2637=CARTESIAN_POINT ( 'NONE',  ( 6.815964470354069604, -1.383691465878164717, -6.173460172893482145 ) ) ;
#2649=ORIENTED_EDGE ( 'NONE', *, *, #622, .F. ) ;
#2654=EDGE_CURVE ( 'NONE', #11133, #488, #3162, .T. ) ;
#2685=EDGE_LOOP ( 'NONE', ( #13978, #10029, #13818, #1557, #12283 ) ) ;
#2698=DIRECTION ( 'NONE',  ( 1.000000000000000000, 0.000000000000000000, 0.000000000000000000 ) ) ;
#2710=CARTESIAN_POINT ( 'NONE',  ( 0.000000000000000000, 0.000000000000000000, 0.000000000000000000 ) ) ;
#2713=LINE ( 'NONE', #14081, #6409 ) ;
#2715=CARTESIAN_POINT ( 'NONE',  ( 6.500000000000000888, 2.536640449112275153, -0.3753468889000217690 ) ) ;
#2717=ORIENTED_EDGE ( 'NONE', *, *, #12846, .T. ) ;
#2727=ADVANCED_FACE ( 'NONE', ( #6341 ), #12991, .T. ) ;
#2736=CARTESIAN_POINT ( 'NONE',  ( 6.500000000000000000, 3.752776749732573247, -0.8000000000000003775 ) ) ;
#2741=CARTESIAN_POINT ( 'NONE',  ( -4.639619758716985842, 4.826867782832376719, -0.1499059597315285375 ) ) ;
#2770=EDGE_CURVE ( 'NONE', #12569, #10525, #6494, .T. ) ;
#2819=CIRCLE ( 'NONE', #7293, 4.000000000000000000 ) ;
#2820=DIRECTION ( 'NONE',  ( -0.5000000000000006661, -0.8660254037844382635, 0.000000000000000000 ) ) ;
#2840=AXIS2_PLACEMENT_3D ( 'NONE', #7240, #9247, #1629 ) ;
#2841=CIRCLE ( 'NONE', #12977, 3.999999999999999112 ) ;
#2860=VERTEX_POINT ( 'NONE', #4494 ) ;
#2881=MECHANICAL_DESIGN_GEOMETRIC_PRESENTATION_REPRESENTATION('',(#9948),#14196);
#2885=ADVANCED_FACE ( 'NONE', ( #8995 ), #4516, .F. ) ;
#2901=EDGE_LOOP ( 'NONE', ( #8125, #3345 ) ) ;
#2911=CARTESIAN_POINT ( 'NONE',  ( 5.589124336233334489, 4.278671059407959554, -6.219623095966918314 ) ) ;
#2927=CARTESIAN_POINT ( 'NONE',  ( 3.399999999999999911, 0.000000000000000000, -7.554475477074173106 ) ) ;
#2936=CARTESIAN_POINT ( 'NONE',  ( 6.837824896291514243, 3.947820044545427454, -6.564402953523716278 ) ) ;
#2968=CARTESIAN_POINT ( 'NONE',  ( -6.500000000000000000, -3.752776749732573247, -0.8000000000000003775 ) ) ;
#2975=ORIENTED_EDGE ( 'NONE', *, *, #1065, .F. ) ;
#3001=CARTESIAN_POINT ( 'NONE',  ( -8.542937654374687995, 0.000000000000000000, -6.800000000000000711 ) ) ;
#3004=VECTOR ( 'NONE', #12514, 1000.000000000000227 ) ;
#3005=CARTESIAN_POINT ( 'NONE',  ( 6.815830331203685866, 0.6619522098568483282, -6.171384342982615401 ) ) ;
#3009=PLANE ( 'NONE',  #1405 ) ;
#3018=APPLICATION_CONTEXT ( 'automotive_design' ) ;
#3027=CARTESIAN_POINT ( 'NONE',  ( 0.000000000000000000, 0.000000000000000000, -7.554475477074173106 ) ) ;
#3062=EDGE_CURVE ( 'NONE', #13769, #14499, #2087, .T. ) ;
#3064=AXIS2_PLACEMENT_3D ( 'NONE', #10610, #9656, #7214 ) ;
#3073=AXIS2_PLACEMENT_3D ( 'NONE', #5283, #13167, #9712 ) ;
#3086=FACE_BOUND ( 'NONE', #2901, .T. ) ;
#3093=CARTESIAN_POINT ( 'NONE',  ( -6.500000000000000000, 3.752776749732564809, -0.7999999999999969358 ) ) ;
#3141=VECTOR ( 'NONE', #615, 1000.000000000000000 ) ;
#3162=B_SPLINE_CURVE_WITH_KNOTS ( 'NONE', 3,
 ( #3471, #1759, #5098, #3916, #8333, #8627 ),
 .UNSPECIFIED., .F., .F.,
 ( 4, 2, 4 ),
 ( 8.673617379884035472E-19, 0.0003352299596267569490, 0.0006704599192535130306 ),
 .UNSPECIFIED. ) ;
#3172=CARTESIAN_POINT ( 'NONE',  ( 0.9108756637647450471, -6.979659189788935514, -6.219623095965384429 ) ) ;
#3193=CARTESIAN_POINT ( 'NONE',  ( -6.826296012759691223, -2.664253980652245168, -6.325071479460635970 ) ) ;
#3206=EDGE_LOOP ( 'NONE', ( #1722, #5625, #10974, #1500, #5620 ) ) ;
#3236=CARTESIAN_POINT ( 'NONE',  ( 6.499999999999999112, -1.280811194704859490, -0.07768058122908397256 ) ) ;
#3248=CARTESIAN_POINT ( 'NONE',  ( -3.399999999999999911, 4.163799117101000559E-16, -8.000000000000000000 ) ) ;
#3256=CARTESIAN_POINT ( 'NONE',  ( -2.241046694639089232, 6.576374040525770681, -6.171384342982497273 ) ) ;
#3273=DIRECTION ( 'NONE',  ( 0.000000000000000000, 0.000000000000000000, -1.000000000000000000 ) ) ;
#3288=ORIENTED_EDGE ( 'NONE', *, *, #14406, .F. ) ;
#3303=CARTESIAN_POINT ( 'NONE',  ( -0.5204879950542059541, -7.205049615410630715, -0.5609245978742286587 ) ) ;
#3332=EDGE_CURVE ( 'NONE', #11582, #1364, #13645, .T. ) ;
#3337=DIRECTION ( 'NONE',  ( -0.000000000000000000, -0.000000000000000000, 1.000000000000000000 ) ) ;
#3340=LINE ( 'NONE', #12328, #446 ) ;
#3341=AXIS2_PLACEMENT_3D ( 'NONE', #9055, #12433, #2187 ) ;
#3345=ORIENTED_EDGE ( 'NONE', *, *, #3332, .F. ) ;
#3360=EDGE_LOOP ( 'NONE', ( #12829, #10464, #1050, #8476, #9983 ) ) ;
#3389=EDGE_LOOP ( 'NONE', ( #13562, #1154, #5348 ) ) ;
#3403=CARTESIAN_POINT ( 'NONE',  ( -6.500000000000002665, -2.501851166488385125, -5.848636054922036642 ) ) ;
#3408=DIRECTION ( 'NONE',  ( -0.000000000000000000, -0.000000000000000000, 1.000000000000000000 ) ) ;
#3409=EDGE_CURVE ( 'NONE', #4509, #4487, #5603, .T. ) ;
#3423=B_SPLINE_CURVE_WITH_KNOTS ( 'NONE', 3,
 ( #9898, #7689, #8799, #13225, #12172, #2968 ),
 .UNSPECIFIED., .F., .F.,
 ( 4, 2, 4 ),
 ( 0.003841072314098365435, 0.005765657563962188134, 0.007690242813826009965 ),
 .UNSPECIFIED. ) ;
#3435=EDGE_CURVE ( 'NONE', #11448, #4487, #5869, .T. ) ;
#3438=CARTESIAN_POINT ( 'NONE',  ( -4.336808689942017736E-16, 7.505553499465137612, -0.8000000000000003775 ) ) ;
#3445=ORIENTED_EDGE ( 'NONE', *, *, #9574, .T. ) ;
#3449=B_SPLINE_CURVE_WITH_KNOTS ( 'NONE', 3,
 ( #13238, #10946, #821, #4234, #8588, #10797, #5196, #7634, #14205, #7332 ),
 .UNSPECIFIED., .F., .F.,
 ( 4, 2, 2, 2, 4 ),
 ( 0.000000000000000000, 0.001989602278884366159, 0.003979204557768732317, 0.005968806836653096741, 0.007958409115537461165 ),
 .UNSPECIFIED. ) ;
#3455=EDGE_CURVE ( 'NONE', #5297, #12569, #1026, .T. ) ;
#3468=CARTESIAN_POINT ( 'NONE',  ( 6.500000000000000000, 3.752776749732564365, -6.177805531629060987 ) ) ;
#3471=CARTESIAN_POINT ( 'NONE',  ( 6.500000000000000000, -3.752776749732574135, -6.064240316920400886 ) ) ;
#3484=ADVANCED_FACE ( 'NONE', ( #11954 ), #7320, .T. ) ;
#3512=ORIENTED_EDGE ( 'NONE', *, *, #8612, .T. ) ;
#3528=ORIENTED_EDGE ( 'NONE', *, *, #4783, .T. ) ;
#3556=EDGE_CURVE ( 'NONE', #11091, #7485, #7993, .T. ) ;
#3557=B_SPLINE_CURVE_WITH_KNOTS ( 'NONE', 3,
 ( #11801, #6130, #10634, #8401, #7301, #1701, #6205, #575 ),
 .UNSPECIFIED., .F., .F.,
 ( 4, 2, 2, 4 ),
 ( 2.459764730742321679E-07, 0.001920659145285711104, 0.002880865729692028403, 0.003841072314098346787 ),
 .UNSPECIFIED. ) ;
#3569=FACE_OUTER_BOUND ( 'NONE', #18, .T. ) ;
#3576=EDGE_CURVE ( 'NONE', #9582, #12254, #2819, .T. ) ;
#3582=VERTEX_POINT ( 'NONE', #14407 ) ;
#3610=ORIENTED_EDGE ( 'NONE', *, *, #8996, .T. ) ;
#3613=ORIENTED_EDGE ( 'NONE', *, *, #859, .F. ) ;
#3641=CARTESIAN_POINT ( 'NONE',  ( -3.250000000000004441, 5.629165124598849879, 0.000000000000000000 ) ) ;
#3645=EDGE_CURVE ( 'NONE', #2860, #4509, #3340, .T. ) ;
#3671=LINE ( 'NONE', #3747, #3141 ) ;
#3682=DIRECTION ( 'NONE',  ( 0.000000000000000000, -1.000000000000000000, 0.000000000000000000 ) ) ;
#3703=CARTESIAN_POINT ( 'NONE',  ( 4.555094537983153558, 5.243183837310242623, -6.208110906918258287 ) ) ;
#3706=ORIENTED_EDGE ( 'NONE', *, *, #14406, .T. ) ;
#3725=B_SPLINE_CURVE_WITH_KNOTS ( 'NONE', 3,
 ( #3728, #9557, #3941, #13765, #8429, #6079, #8138, #12644, #4839, #12723 ),
 .UNSPECIFIED., .F., .F.,
 ( 4, 2, 2, 2, 4 ),
 ( 0.000000000000000000, 0.001989602278884364858, 0.003979204557768729715, 0.005968806836653094139, 0.007958409115537459430 ),
 .UNSPECIFIED. ) ;
#3728=CARTESIAN_POINT ( 'NONE',  ( -6.837824896291514243, 3.947820044545427454, -6.564402953523716278 ) ) ;
#3742=CARTESIAN_POINT ( 'NONE',  ( 6.500000000000000000, -1.417018949932591365, -5.722407714414702085 ) ) ;
#3747=CARTESIAN_POINT ( 'NONE',  ( -6.500000000000000000, -3.752776749732572803, -8.000000000000000000 ) ) ;
#3749=CARTESIAN_POINT ( 'NONE',  ( 2.133938722758552675, 6.273523403446317204, -0.09463688534106567962 ) ) ;
#3760=EDGE_CURVE ( 'NONE', #1120, #8086, #11584, .T. ) ;
#3774=B_SPLINE_CURVE_WITH_KNOTS ( 'NONE', 3,
 ( #7546, #1935, #8802, #12175, #9978, #13523, #3703, #12624, #204, #9019 ),
 .UNSPECIFIED., .F., .F.,
 ( 4, 2, 2, 2, 4 ),
 ( 8.662740229329108052E-20, 0.001989602278884365725, 0.003979204557768730582, 0.005968806836653095874, 0.007958409115537461165 ),
 .UNSPECIFIED. ) ;
#3786=EDGE_CURVE ( 'NONE', #14203, #5297, #538, .T. ) ;
#3807=CARTESIAN_POINT ( 'NONE',  ( 6.270061300899935297, -4.268872906156509828, -6.443866470201760954 ) ) ;
#3830=CARTESIAN_POINT ( 'NONE',  ( 0.5204879950541921874, 7.205049615410631603, -0.5609245978742269934 ) ) ;
#3834=EDGE_CURVE ( 'NONE', #12569, #6919, #2306, .T. ) ;
#3843=CARTESIAN_POINT ( 'NONE',  ( -5.357619327558935599E-16, 7.505553499465137612, -6.177802698399959880 ) ) ;
#3890=DIRECTION ( 'NONE',  ( 0.000000000000000000, 0.000000000000000000, -1.000000000000000000 ) ) ;
#3905=CARTESIAN_POINT ( 'NONE',  ( 6.815830331203685866, 1.228021141713631082E-13, -6.171384342982610960 ) ) ;
#3916=CARTESIAN_POINT ( 'NONE',  ( 6.663127973346360200, -3.846958729056453308, -6.460793508093580328 ) ) ;
#3932=CARTESIAN_POINT ( 'NONE',  ( -1.083333333333333037, -6.880090707843053544, -5.848636054922041083 ) ) ;
#3933=EDGE_CURVE ( 'NONE', #8797, #12920, #3557, .T. ) ;
#3940=FACE_OUTER_BOUND ( 'NONE', #11238, .T. ) ;
#3941=CARTESIAN_POINT ( 'NONE',  ( -5.698650001973517121, 4.592339236403562452, -6.344532336093705815 ) ) ;
#3953=CARTESIAN_POINT ( 'NONE',  ( 1.083333333333333703, 6.880090707843044662, -5.848636054922036642 ) ) ;
#3957=DIRECTION ( 'NONE',  ( 0.000000000000000000, 0.000000000000000000, 1.000000000000000000 ) ) ;
#3970=CARTESIAN_POINT ( 'NONE',  ( -6.500000000000000000, 3.752776749732564809, -6.064240316920399110 ) ) ;
#4014=CARTESIAN_POINT ( 'NONE',  ( 1.098735407079667992, 7.248058225760153128, -6.326622577870739228 ) ) ;
#4037=CARTESIAN_POINT ( 'NONE',  ( 6.500000000000000888, 4.077976443323007238, -6.122137821720842865 ) ) ;
#4039=CARTESIAN_POINT ( 'NONE',  ( 0.000000000000000000, 0.000000000000000000, -6.800000000000000711 ) ) ;
#4054=EDGE_CURVE ( 'NONE', #12397, #6727, #7540, .T. ) ;
#4057=DIRECTION ( 'NONE',  ( 0.000000000000000000, 0.000000000000000000, -1.000000000000000000 ) ) ;
#4061=CARTESIAN_POINT ( 'NONE',  ( 6.500000000000000000, 3.453380256388213887, -0.6809028088495826525 ) ) ;
#4136=ORIENTED_EDGE ( 'NONE', *, *, #4337, .T. ) ;
#4164=ORIENTED_EDGE ( 'NONE', *, *, #8352, .F. ) ;
#4170=EDGE_LOOP ( 'NONE', ( #9110, #12012 ) ) ;
#4176=AXIS2_PLACEMENT_3D ( 'NONE', #7828, #13569, #9222 ) ;
#4184=VECTOR ( 'NONE', #9342, 999.9999999999998863 ) ;
#4186=CARTESIAN_POINT ( 'NONE',  ( -3.250000000000004441, 5.629165124598849879, 0.000000000000000000 ) ) ;
#4196=CARTESIAN_POINT ( 'NONE',  ( -6.500000000000000888, 0.000000000000000000, 0.000000000000000000 ) ) ;
#4229=CARTESIAN_POINT ( 'NONE',  ( -6.500000000000000000, -1.336926445777093964, -6.054363369342815382 ) ) ;
#4234=CARTESIAN_POINT ( 'NONE',  ( -2.262848203703084593, -6.566616684922157887, -6.208169345099794789 ) ) ;
#4241=EDGE_LOOP ( 'NONE', ( #6674, #9406, #1655, #7629, #7207 ) ) ;
#4243=B_SPLINE_CURVE_WITH_KNOTS ( 'NONE', 3,
 ( #6370, #8168, #13568, #184, #6929, #11209 ),
 .UNSPECIFIED., .F., .F.,
 ( 4, 2, 4 ),
 ( 0.003981881017442828914, 0.005970145066490142871, 0.007958409115537457695 ),
 .UNSPECIFIED. ) ;
#4263=EDGE_CURVE ( 'NONE', #12176, #5143, #11440, .T. ) ;
#4286=CONICAL_SURFACE ( 'NONE', #13467, 3.999999999999999112, 0.9599310885968813656 ) ;
#4288=PRODUCT_DEFINITION_CONTEXT ( 'detailed design', #9333, 'design' ) ;
#4305=ADVANCED_FACE ( 'NONE', ( #6252 ), #9428, .T. ) ;
#4306=AXIS2_PLACEMENT_3D ( 'NONE', #12833, #10755, #633 ) ;
#4307=CARTESIAN_POINT ( 'NONE',  ( -6.838238953609876880, 3.993985489099932007, -6.572971244646267586 ) ) ;
#4309=EDGE_LOOP ( 'NONE', ( #2457, #9771, #1731 ) ) ;
#4321=EDGE_CURVE ( 'NONE', #2113, #151, #6602, .T. ) ;
#4327=CARTESIAN_POINT ( 'NONE',  ( 6.500000000000000000, -3.752776749732574135, -6.064240316920400886 ) ) ;
#4329=DIRECTION ( 'NONE',  ( 0.000000000000000000, 0.000000000000000000, -1.000000000000000000 ) ) ;
#4337=EDGE_CURVE ( 'NONE', #6378, #2860, #12329, .T. ) ;
#4347=CARTESIAN_POINT ( 'NONE',  ( 0.000000000000000000, 0.000000000000000000, 0.000000000000000000 ) ) ;
#4359=CARTESIAN_POINT ( 'NONE',  ( 6.878751942472531411, 3.924677726130922473, -6.573129608219089981 ) ) ;
#4372=CARTESIAN_POINT ( 'NONE',  ( -5.619193549421041212, 4.261310591078285803, -5.875704392894027350 ) ) ;
#4373=ORIENTED_EDGE ( 'NONE', *, *, #7319, .F. ) ;
#4378=DIRECTION ( 'NONE',  ( 1.000000000000000000, 0.000000000000000000, 0.000000000000000000 ) ) ;
#4423=CARTESIAN_POINT ( 'NONE',  ( 2.075968632158072591, 6.306992450858666110, -6.056431503347234013 ) ) ;
#4426=ORIENTED_EDGE ( 'NONE', *, *, #9906, .F. ) ;
#4427=CARTESIAN_POINT ( 'NONE',  ( -2.075968632161005800, -6.306992450858350807, -6.056431503346042078 ) ) ;
#4432=AXIS2_PLACEMENT_3D ( 'NONE', #12803, #8428, #9331 ) ;
#4477=FACE_OUTER_BOUND ( 'NONE', #6259, .T. ) ;
#4481=EDGE_LOOP ( 'NONE', ( #4754, #13739, #9861, #13102 ) ) ;
#4487=VERTEX_POINT ( 'NONE', #4186 ) ;
#4494=CARTESIAN_POINT ( 'NONE',  ( -6.500000000000000000, 3.752776749732564809, -6.064240316920399110 ) ) ;
#4497=ADVANCED_FACE ( 'NONE', ( #4477 ), #9909, .T. ) ;
#4499=CARTESIAN_POINT ( 'NONE',  ( 6.500000000000000888, 0.000000000000000000, 0.000000000000000000 ) ) ;
#4509=VERTEX_POINT ( 'NONE', #9863 ) ;
#4515=FACE_BOUND ( 'NONE', #6586, .T. ) ;
#4516=( BOUNDED_SURFACE ( )  B_SPLINE_SURFACE ( 3, 2, ( 
 ( #10982, #5377, #9877 ),
 ( #13281, #3172, #7675 ),
 ( #12157, #2040, #6559 ),
 ( #7949, #8097, #12444 ),
 ( #6767, #12530, #10311 ),
 ( #1464, #1309, #5670 ) ),
 .UNSPECIFIED., .F., .F., .F. ) 
 B_SPLINE_SURFACE_WITH_KNOTS ( ( 4, 2, 4 ),
 ( 3, 3 ),
 ( 0.003190620565844226857, 0.007281897438794493645, 0.01137317431174476000 ),
 ( 0.000000000000000000, 1.000000000000000000 ),
 .UNSPECIFIED. ) 
 GEOMETRIC_REPRESENTATION_ITEM ( )  RATIONAL_B_SPLINE_SURFACE ( (
 ( 1.000000000000000000, 0.8047731410850399447, 1.000000000000000000),
 ( 1.000000000000000000, 0.8125552299147021929, 1.000000000000000000),
 ( 1.000000000000000000, 0.8191520442902128218, 1.000000000000000000),
 ( 1.000000000000000000, 0.8191520442877616714, 1.000000000000000000),
 ( 1.000000000000000000, 0.8125552299165426096, 1.000000000000000000),
 ( 1.000000000000000000, 0.8047731410850402778, 1.000000000000000000) ) ) 
 REPRESENTATION_ITEM ( '' )  SURFACE ( )  );
#4526=DIRECTION ( 'NONE',  ( -1.000000000000000000, 0.000000000000000000, 0.000000000000000000 ) ) ;
#4557=SHAPE_REPRESENTATION_RELATIONSHIP ( 'NONE' , 'NONE' ,  #1780, #4558 ) ;
#4558=ADVANCED_BREP_SHAPE_REPRESENTATION ( '', ( #12340, #9440 ), #13250 ) ;
#4559=FACE_OUTER_BOUND ( 'NONE', #12030, .T. ) ;
#4570=DIRECTION ( 'NONE',  ( 1.000000000000000000, 0.000000000000000000, 0.000000000000000000 ) ) ;
#4578=ADVANCED_FACE ( 'NONE', ( #4559 ), #10136, .T. ) ;
#4582=VERTEX_POINT ( 'NONE', #3438 ) ;
#4596=DIRECTION ( 'NONE',  ( -1.000000000000000000, 0.000000000000000000, 0.000000000000000000 ) ) ;
#4625=DIRECTION ( 'NONE',  ( 0.000000000000000000, 0.000000000000000000, 1.000000000000000000 ) ) ;
#4637=B_SPLINE_CURVE_WITH_KNOTS ( 'NONE', 3,
 ( #10501, #3807, #11457, #454, #7116, #5851, #228, #4772, #8134, #9259 ),
 .UNSPECIFIED., .F., .F.,
 ( 4, 2, 2, 2, 4 ),
 ( 0.000000000000000000, 0.001989602278884365291, 0.003979204557768730582, 0.005968806836653095874, 0.007958409115537461165 ),
 .UNSPECIFIED. ) ;
#4655=FACE_OUTER_BOUND ( 'NONE', #4170, .T. ) ;
#4663=CARTESIAN_POINT ( 'NONE',  ( -6.500000000000000000, -3.752776749732572803, -6.064240316920399998 ) ) ;
#4692=CARTESIAN_POINT ( 'NONE',  ( -4.000000000000000000, 4.898587196589412829E-16, -8.000000000000000000 ) ) ;
#4702=B_SPLINE_CURVE_WITH_KNOTS ( 'NONE', 3,
 ( #2389, #6605, #12349, #6, #2085, #10284 ),
 .UNSPECIFIED., .F., .F.,
 ( 4, 2, 4 ),
 ( 0.003841072314098346787, 0.005765657563962181195, 0.007690242813826015170 ),
 .UNSPECIFIED. ) ;
#4732=DIRECTION ( 'NONE',  ( 0.000000000000000000, 0.000000000000000000, -1.000000000000000000 ) ) ;
#4736=DIRECTION ( 'NONE',  ( 1.000000000000000000, 0.000000000000000000, 0.000000000000000000 ) ) ;
#4749=EDGE_CURVE ( 'NONE', #13126, #4582, #6088, .T. ) ;
#4752=UNCERTAINTY_MEASURE_WITH_UNIT (LENGTH_MEASURE( 1.000000000000000082E-05 ), #12400, 'distance_accuracy_value', 'NONE');
#4754=ORIENTED_EDGE ( 'NONE', *, *, #3576, .T. ) ;
#4772=CARTESIAN_POINT ( 'NONE',  ( 1.126429428730187032, -7.232124035235040438, -6.344710093416088270 ) ) ;
#4783=EDGE_CURVE ( 'NONE', #1364, #11582, #2841, .T. ) ;
#4823=CARTESIAN_POINT ( 'NONE',  ( -2.141486166123589996, 6.269165884987821791, -0.07763482564820804732 ) ) ;
#4839=CARTESIAN_POINT ( 'NONE',  ( -0.5620262070071414540, 7.564407249984292037, -6.443844059477446429 ) ) ;
#4850=CARTESIAN_POINT ( 'NONE',  ( 3.339999999999998970, 0.000000000000000000, -0.4621369752184044666 ) ) ;
#4855=CARTESIAN_POINT ( 'NONE',  ( 6.500000000000001776, -4.012858516023013244, -6.470130706010830401 ) ) ;
#4873=CARTESIAN_POINT ( 'NONE',  ( 6.499999999999997335, 1.286902272306391870, -0.09436334093186085625 ) ) ;
#4909=CYLINDRICAL_SURFACE ( 'NONE', #4432, 4.000000000000000000 ) ;
#4912=DIRECTION ( 'NONE',  ( 0.000000000000000000, 0.000000000000000000, 1.000000000000000000 ) ) ;
#4934=AXIS2_PLACEMENT_3D ( 'NONE', #12860, #9173, #13899 ) ;
#4937=B_SPLINE_CURVE_WITH_KNOTS ( 'NONE', 3,
 ( #4196, #13125, #1825, #8557, #8623, #13063, #1908, #6421, #10921, #3093 ),
 .UNSPECIFIED., .F., .F.,
 ( 4, 2, 2, 2, 4 ),
 ( 0.009353627468483380336, 0.01031000219096067302, 0.01126637691343796571, 0.01222275163591525840, 0.01317912635839255109 ),
 .UNSPECIFIED. ) ;
#4951=EDGE_CURVE ( 'NONE', #1897, #2224, #2134, .T. ) ;
#4955=DIRECTION ( 'NONE',  ( -0.8660254037844382635, -0.5000000000000006661, 0.000000000000000000 ) ) ;
#4956=FACE_OUTER_BOUND ( 'NONE', #6783, .T. ) ;
#4989=DIRECTION ( 'NONE',  ( 0.000000000000000000, 0.000000000000000000, -1.000000000000000000 ) ) ;
#5019=DIRECTION ( 'NONE',  ( 1.000000000000000000, 0.000000000000000000, 0.000000000000000000 ) ) ;
#5022=EDGE_LOOP ( 'NONE', ( #2399, #11250, #6023, #11449 ) ) ;
#5023=DIRECTION ( 'NONE',  ( -0.000000000000000000, -0.000000000000000000, 1.000000000000000000 ) ) ;
#5025=CARTESIAN_POINT ( 'NONE',  ( 6.500000000000000000, 3.149025070564758888, -0.5705737632551094451 ) ) ;
#5067=CARTESIAN_POINT ( 'NONE',  ( 5.978033218201114884, 4.054134411712192687, -0.5602453477493293255 ) ) ;
#5073=CARTESIAN_POINT ( 'NONE',  ( 3.250000000000000444, 5.629165124598851655, -5.592027715088707218 ) ) ;
#5079=ORIENTED_EDGE ( 'NONE', *, *, #4321, .F. ) ;
#5084=CARTESIAN_POINT ( 'NONE',  ( -6.837824896291514243, 3.947820044545427454, -6.564402953523716278 ) ) ;
#5098=CARTESIAN_POINT ( 'NONE',  ( 6.539198257602126141, -3.775407874310924505, -6.286450516131050215 ) ) ;
#5130=EDGE_CURVE ( 'NONE', #9582, #6727, #9674, .T. ) ;
#5143=VERTEX_POINT ( 'NONE', #14032 ) ;
#5154=CARTESIAN_POINT ( 'NONE',  ( -8.331345277524542681, 1.020295532671184640E-15, -7.381345277524544279 ) ) ;
#5174=DIRECTION ( 'NONE',  ( -1.000000000000000000, 0.000000000000000000, 0.000000000000000000 ) ) ;
#5177=DIRECTION ( 'NONE',  ( 0.9396926207859143121, 1.150791560227857665E-16, -0.3420201433256525592 ) ) ;
#5183=CIRCLE ( 'NONE', #14369, 0.6186547224754559426 ) ;
#5196=CARTESIAN_POINT ( 'NONE',  ( -4.555094537983154446, -5.243183837310248840, -6.208110906918257399 ) ) ;
#5239=EDGE_CURVE ( 'NONE', #12920, #12815, #7601, .T. ) ;
#5250=EDGE_CURVE ( 'NONE', #8797, #12815, #1296, .T. ) ;
#5253=DIRECTION ( 'NONE',  ( -0.000000000000000000, -0.000000000000000000, 1.000000000000000000 ) ) ;
#5267=CARTESIAN_POINT ( 'NONE',  ( -6.500000000000000000, -3.752776749732572803, -8.000000000000000000 ) ) ;
#5283=CARTESIAN_POINT ( 'NONE',  ( 0.000000000000000000, 0.000000000000000000, -0.4201245229258211977 ) ) ;
#5297=VERTEX_POINT ( 'NONE', #12670 ) ;
#5306=DIRECTION ( 'NONE',  ( 0.000000000000000000, 0.000000000000000000, -1.000000000000000000 ) ) ;
#5307=DIRECTION ( 'NONE',  ( -1.000000000000000000, 0.000000000000000000, 0.000000000000000000 ) ) ;
#5320=DIRECTION ( 'NONE',  ( -0.000000000000000000, -0.000000000000000000, 1.000000000000000000 ) ) ;
#5329=B_SPLINE_CURVE_WITH_KNOTS ( 'NONE', 3,
 ( #6064, #360, #2604, #11386, #9250, #12481 ),
 .UNSPECIFIED., .F., .F.,
 ( 4, 2, 4 ),
 ( 0.003981881017442818506, 0.005970145066490139402, 0.007958409115537461165 ),
 .UNSPECIFIED. ) ;
#5331=CARTESIAN_POINT ( 'NONE',  ( -6.781345014477444977, 3.590342129888853151, -6.122077150241850951 ) ) ;
#5334=CARTESIAN_POINT ( 'NONE',  ( -6.500000000000000000, 1.392044006191029304, -6.058542048163745086 ) ) ;
#5335=EDGE_LOOP ( 'NONE', ( #1341, #7757, #340 ) ) ;
#5348=ORIENTED_EDGE ( 'NONE', *, *, #3409, .F. ) ;
#5349=EDGE_CURVE ( 'NONE', #14499, #8855, #14400, .T. ) ;
#5360=ORIENTED_EDGE ( 'NONE', *, *, #8291, .T. ) ;
#5362=DIRECTION ( 'NONE',  ( -1.000000000000000000, 0.000000000000000000, 0.000000000000000000 ) ) ;
#5377=CARTESIAN_POINT ( 'NONE',  ( -0.2259792476677704443, -7.636022678937404606, -6.470294263593365791 ) ) ;
#5379=VECTOR ( 'NONE', #1125, 1000.000000000000000 ) ;
#5381=DIRECTION ( 'NONE',  ( 0.000000000000000000, 0.000000000000000000, 1.000000000000000000 ) ) ;
#5401=CARTESIAN_POINT ( 'NONE',  ( 0.000000000000000000, 0.000000000000000000, -8.000000000000000000 ) ) ;
#5417=CONICAL_SURFACE ( 'NONE', #2586, 6.500000000000000888, 0.8987552595851582282 ) ;
#5427=ORIENTED_EDGE ( 'NONE', *, *, #3435, .T. ) ;
#5448=CARTESIAN_POINT ( 'NONE',  ( -12.99999999999999112, -3.903127820947815962E-15, 0.000000000000000000 ) ) ;
#5525=CARTESIAN_POINT ( 'NONE',  ( -3.755786496842903988E-16, -7.505553499465146494, -8.000000000000000000 ) ) ;
#5538=CARTESIAN_POINT ( 'NONE',  ( -6.500000000000000000, 3.752776749732564809, -6.064240316920399110 ) ) ;
#5543=CARTESIAN_POINT ( 'NONE',  ( 0.000000000000000000, 0.000000000000000000, -7.554475477074173106 ) ) ;
#5567=PRODUCT ( 'hex flange nut gradea_iso_ISO - 4161 - M8 - N', 'hex flange nut gradea_iso_ISO - 4161 - M8 - N', '', ( #655 ) ) ;
#5599=CARTESIAN_POINT ( 'NONE',  ( 3.250000000000004441, 5.629165124598849879, 0.000000000000000000 ) ) ;
#5600=CARTESIAN_POINT ( 'NONE',  ( 8.331345277524542681, 0.000000000000000000, -8.000000000000000000 ) ) ;
#5603=B_SPLINE_CURVE_WITH_KNOTS ( 'NONE', 3,
 ( #6957, #9253, #7247, #2741, #13982, #9394, #13821, #2455 ),
 .UNSPECIFIED., .F., .F.,
 ( 4, 2, 2, 4 ),
 ( 2.459764730722484167E-07, 0.001920659145285713056, 0.002880865729692032307, 0.003841072314098351557 ),
 .UNSPECIFIED. ) ;
#5620=ORIENTED_EDGE ( 'NONE', *, *, #7667, .T. ) ;
#5625=ORIENTED_EDGE ( 'NONE', *, *, #2363, .T. ) ;
#5641=EDGE_LOOP ( 'NONE', ( #6120, #797, #86, #11288 ) ) ;
#5658=DIRECTION ( 'NONE',  ( -0.8191520442889923537, 1.003171929053525363E-16, 0.5735764363510453823 ) ) ;
#5670=CARTESIAN_POINT ( 'NONE',  ( 6.878751942472530523, -3.924677726130933575, -6.573129608219091757 ) ) ;
#5674=AXIS2_PLACEMENT_3D ( 'NONE', #12228, #5381, #7951 ) ;
#5685=CARTESIAN_POINT ( 'NONE',  ( -2.055025722541619970, -6.319083845364135144, -5.720331885005373707 ) ) ;
#5731=CARTESIAN_POINT ( 'NONE',  ( -3.339999999999998970, 4.090320309152158050E-16, -0.4621369752184044666 ) ) ;
#5749=DIRECTION ( 'NONE',  ( -0.8660254037844382635, 0.5000000000000005551, 0.000000000000000000 ) ) ;
#5754=CARTESIAN_POINT ( 'NONE',  ( -0.8808064505793390397, -6.997019658119205232, -5.875704392894199657 ) ) ;
#5770=CARTESIAN_POINT ( 'NONE',  ( -4.336808689942017736E-16, 7.505553499465137612, -0.8000000000000003775 ) ) ;
#5786=CARTESIAN_POINT ( 'NONE',  ( 6.837824896291514243, 3.947820044545427454, -6.564402953523716278 ) ) ;
#5799=CARTESIAN_POINT ( 'NONE',  ( -1.860380241283027480, -6.431462466365327479, -0.1499059597315341996 ) ) ;
#5812=CARTESIAN_POINT ( 'NONE',  ( -3.999999999999999112, 4.898587196589411843E-16, 3.469446951953614189E-15 ) ) ;
#5830=EDGE_CURVE ( 'NONE', #11091, #6727, #9117, .T. ) ;
#5851=CARTESIAN_POINT ( 'NONE',  ( 2.837346585668845567, -6.232092946297389524, -6.171287963165198676 ) ) ;
#5857=VECTOR ( 'NONE', #12223, 1000.000000000000000 ) ;
#5869=CIRCLE ( 'NONE', #14126, 6.500000000000000888 ) ;
#5877=DIRECTION ( 'NONE',  ( 1.000000000000000000, 0.000000000000000000, 0.000000000000000000 ) ) ;
#5878=ORIENTED_EDGE ( 'NONE', *, *, #5250, .T. ) ;
#5893=EDGE_CURVE ( 'NONE', #2224, #1364, #10455, .T. ) ;
#5917=CARTESIAN_POINT ( 'NONE',  ( -2.690931834596280936, 5.951943280390038282, 1.006275141338108408E-15 ) ) ;
#5927=CIRCLE ( 'NONE', #3073, 3.399999999999999911 ) ;
#5948=ADVANCED_FACE ( 'NONE', ( #12813 ), #9605, .T. ) ;
#5971=CARTESIAN_POINT ( 'NONE',  ( -6.500000000000000888, 0.000000000000000000, 0.000000000000000000 ) ) ;
#5975=DIRECTION ( 'NONE',  ( 1.000000000000000000, 0.000000000000000000, 0.000000000000000000 ) ) ;
#6023=ORIENTED_EDGE ( 'NONE', *, *, #2654, .F. ) ;
#6024=EDGE_CURVE ( 'NONE', #5143, #488, #5329, .T. ) ;
#6027=DIRECTION ( 'NONE',  ( 1.000000000000000000, 0.000000000000000000, 0.000000000000000000 ) ) ;
#6030=CARTESIAN_POINT ( 'NONE',  ( 8.331345277524542681, 0.000000000000000000, -7.381345277524544279 ) ) ;
#6035=CARTESIAN_POINT ( 'NONE',  ( -6.500000000000000000, -3.752776749732573247, -0.8000000000000003775 ) ) ;
#6052=CARTESIAN_POINT ( 'NONE',  ( 6.837824896291514243, -3.947820044545437224, -6.564402953523717166 ) ) ;
#6064=CARTESIAN_POINT ( 'NONE',  ( 6.815830331203685866, 1.228021141713631082E-13, -6.171384342982610960 ) ) ;
#6076=CARTESIAN_POINT ( 'NONE',  ( -6.837824896291515131, -3.947820044545435447, -6.564402953523717166 ) ) ;
#6079=CARTESIAN_POINT ( 'NONE',  ( -2.837346585668847787, 6.232092946297378866, -6.171287963165196899 ) ) ;
#6088=LINE ( 'NONE', #14134, #11558 ) ;
#6104=( BOUNDED_SURFACE ( )  B_SPLINE_SURFACE ( 3, 2, ( 
 ( #6860, #12456, #11212 ),
 ( #2495, #7833, #12385 ),
 ( #2269, #6997, #11496 ),
 ( #5685, #4427, #13512 ),
 ( #5754, #6780, #8109 ),
 ( #11285, #1391, #12613 ) ),
 .UNSPECIFIED., .F., .F., .T. ) 
 B_SPLINE_SURFACE_WITH_KNOTS ( ( 4, 2, 4 ),
 ( 3, 3 ),
 ( 0.003190620565844225990, 0.007281897438794491043, 0.01137317431174475653 ),
 ( 0.000000000000000000, 1.000000000000000000 ),
 .UNSPECIFIED. ) 
 GEOMETRIC_REPRESENTATION_ITEM ( )  RATIONAL_B_SPLINE_SURFACE ( (
 ( 1.000000000000000000, 0.8047731410850402778, 1.000000000000000000),
 ( 1.000000000000000000, 0.8125552299156234559, 1.000000000000000000),
 ( 1.000000000000000000, 0.8191520442889865805, 1.000000000000000000),
 ( 1.000000000000000000, 0.8191520442889865805, 1.000000000000000000),
 ( 1.000000000000000000, 0.8125552299156227898, 1.000000000000000000),
 ( 1.000000000000000000, 0.8047731410850399447, 1.000000000000000000) ) ) 
 REPRESENTATION_ITEM ( '' )  SURFACE ( )  );
#6120=ORIENTED_EDGE ( 'NONE', *, *, #5830, .F. ) ;
#6130=CARTESIAN_POINT ( 'NONE',  ( 5.979512004945807924, -4.053280633787082365, -0.5609245978742287697 ) ) ;
#6142=AXIS2_PLACEMENT_3D ( 'NONE', #89, #2405, #2470 ) ;
#6179=CARTESIAN_POINT ( 'NONE',  ( 0.000000000000000000, 0.000000000000000000, -6.800000000000000711 ) ) ;
#6205=CARTESIAN_POINT ( 'NONE',  ( 3.528928113779637776, -5.468125903023631551, -5.911160594572010107E-15 ) ) ;
#6212=CLOSED_SHELL ( 'NONE', ( #7208, #10728, #833, #6466, #13129, #7909, #8020, #2727, #11590, #364, #782, #3484, #6318, #13409, #8369, #4578, #6372, #10840, #785, #4497, #4305, #5948, #13511, #2005, #2885, #282, #13851, #9822, #11354, #11483, #12335, #6713 ) ) ;
#6217=EDGE_CURVE ( 'NONE', #10525, #151, #8370, .T. ) ;
#6232=CARTESIAN_POINT ( 'NONE',  ( 6.500000000000000000, 3.752776749732573247, -0.8000000000000003775 ) ) ;
#6247=ORIENTED_EDGE ( 'NONE', *, *, #3933, .F. ) ;
#6252=FACE_OUTER_BOUND ( 'NONE', #3389, .T. ) ;
#6259=EDGE_LOOP ( 'NONE', ( #5079, #6766, #1519 ) ) ;
#6278=ORIENTED_EDGE ( 'NONE', *, *, #5893, .F. ) ;
#6310=ORIENTED_EDGE ( 'NONE', *, *, #3556, .F. ) ;
#6318=ADVANCED_FACE ( 'NONE', ( #12818 ), #553, .T. ) ;
#6341=FACE_OUTER_BOUND ( 'NONE', #13786, .T. ) ;
#6347=AXIS2_PLACEMENT_3D ( 'NONE', #5543, #3408, #4596 ) ;
#6369=FACE_OUTER_BOUND ( 'NONE', #10614, .T. ) ;
#6370=CARTESIAN_POINT ( 'NONE',  ( -6.815830331203685866, -1.210827632163352847E-13, -6.171384342982610960 ) ) ;
#6372=ADVANCED_FACE ( 'NONE', ( #9347 ), #14326, .T. ) ;
#6378=VERTEX_POINT ( 'NONE', #1522 ) ;
#6409=VECTOR ( 'NONE', #5023, 1000.000000000000000 ) ;
#6417=DIRECTION ( 'NONE',  ( 1.000000000000000000, 0.000000000000000000, 0.000000000000000000 ) ) ;
#6421=CARTESIAN_POINT ( 'NONE',  ( -6.500000000000000000, 3.149025070564754003, -0.5705737632551073357 ) ) ;
#6466=ADVANCED_FACE ( 'NONE', ( #692 ), #395, .T. ) ;
#6494=LINE ( 'NONE', #5525, #5857 ) ;
#6499=CARTESIAN_POINT ( 'NONE',  ( -6.837824896291515131, -3.947820044545435447, -6.564402953523717166 ) ) ;
#6500=ORIENTED_EDGE ( 'NONE', *, *, #3576, .F. ) ;
#6532=CARTESIAN_POINT ( 'NONE',  ( 6.500000000000000888, 2.679956093905413450, -6.238387772031967593 ) ) ;
#6543=AXIS2_PLACEMENT_3D ( 'NONE', #10673, #3890, #546 ) ;
#6553=EDGE_LOOP ( 'NONE', ( #3610, #11927, #1136, #6278 ) ) ;
#6559=CARTESIAN_POINT ( 'NONE',  ( 2.241046694638796133, -6.576374040525796438, -6.171384342982452864 ) ) ;
#6585=CARTESIAN_POINT ( 'NONE',  ( -6.500000000000000888, -4.077972562205394169, -6.122137109124704324 ) ) ;
#6586=EDGE_LOOP ( 'NONE', ( #6500, #14210 ) ) ;
#6591=( NAMED_UNIT ( * ) PLANE_ANGLE_UNIT ( ) SI_UNIT ( $, .RADIAN. ) );
#6600=CIRCLE ( 'NONE', #926, 6.500000000000000888 ) ;
#6602=CIRCLE ( 'NONE', #6829, 6.500000000000000888 ) ;
#6605=CARTESIAN_POINT ( 'NONE',  ( 2.690931834596283156, -5.951943280390046276, -5.793705359219412742E-15 ) ) ;
#6612=AXIS2_PLACEMENT_3D ( 'NONE', #14475, #1094, #6865 ) ;
#6642=CARTESIAN_POINT ( 'NONE',  ( 6.499999999999999112, -3.752776749732576356, -0.8000000000000003775 ) ) ;
#6674=ORIENTED_EDGE ( 'NONE', *, *, #3645, .F. ) ;
#6710=CARTESIAN_POINT ( 'NONE',  ( 5.619193549421086509, 4.261310591078260046, -5.875704392893767114 ) ) ;
#6713=ADVANCED_FACE ( 'NONE', ( #3940 ), #4909, .F. ) ;
#6727=VERTEX_POINT ( 'NONE', #12643 ) ;
#6731=EDGE_CURVE ( 'NONE', #11133, #8797, #1649, .T. ) ;
#6747=CARTESIAN_POINT ( 'NONE',  ( 0.000000000000000000, 0.000000000000000000, -6.800000000000000711 ) ) ;
#6749=ORIENTED_EDGE ( 'NONE', *, *, #6974, .T. ) ;
#6766=ORIENTED_EDGE ( 'NONE', *, *, #11574, .F. ) ;
#6767=CARTESIAN_POINT ( 'NONE',  ( 5.619193549421182432, -4.261310591078213861, -5.875704392892080463 ) ) ;
#6780=CARTESIAN_POINT ( 'NONE',  ( -0.9108756637647318355, -6.979659189790606177, -6.219623095965800097 ) ) ;
#6783=EDGE_LOOP ( 'NONE', ( #4136, #13928, #3613, #11835 ) ) ;
#6785=CARTESIAN_POINT ( 'NONE',  ( 6.746887896521065464, 3.895317543251747061, -6.526184258131188187 ) ) ;
#6829=AXIS2_PLACEMENT_3D ( 'NONE', #2710, #11777, #5019 ) ;
#6860=CARTESIAN_POINT ( 'NONE',  ( -6.781345014477444977, -3.590342129888860256, -6.122077150241852728 ) ) ;
#6865=DIRECTION ( 'NONE',  ( 1.000000000000000000, 0.000000000000000000, -0.000000000000000000 ) ) ;
#6887=PRODUCT_DEFINITION_FORMATION_WITH_SPECIFIED_SOURCE ( 'ANY', '', #5567, .NOT_KNOWN. ) ;
#6899=EDGE_CURVE ( 'NONE', #6919, #14203, #3449, .T. ) ;
#6919=VERTEX_POINT ( 'NONE', #11007 ) ;
#6929=CARTESIAN_POINT ( 'NONE',  ( -6.831985876597697072, 3.295913427296342402, -6.443925148804115821 ) ) ;
#6939=ORIENTED_EDGE ( 'NONE', *, *, #3409, .T. ) ;
#6957=CARTESIAN_POINT ( 'NONE',  ( -6.500000000000000000, 3.752776749732564809, -0.7999999999999969358 ) ) ;
#6974=EDGE_CURVE ( 'NONE', #12815, #11448, #13891, .T. ) ;
#6991=CARTESIAN_POINT ( 'NONE',  ( -6.500000000000000000, -3.155218591052673549, -0.5622968210053901350 ) ) ;
#6997=CARTESIAN_POINT ( 'NONE',  ( -4.424031367838992423, -4.951337798339370266, -6.056431503346042078 ) ) ;
#7003=ORIENTED_EDGE ( 'NONE', *, *, #4054, .F. ) ;
#7040=ORIENTED_EDGE ( 'NONE', *, *, #8420, .T. ) ;
#7069=CARTESIAN_POINT ( 'NONE',  ( -6.500000000000000000, -3.752776749732573247, -0.8000000000000003775 ) ) ;
#7083=CARTESIAN_POINT ( 'NONE',  ( -1.098735407080685844, 7.248058225761802476, -6.326622577871337860 ) ) ;
#7116=CARTESIAN_POINT ( 'NONE',  ( 3.983107665916332252, -5.570601890521292177, -6.171481112545254000 ) ) ;
#7118=DIRECTION ( 'NONE',  ( -1.000000000000000000, 0.000000000000000000, 0.000000000000000000 ) ) ;
#7134=CARTESIAN_POINT ( 'NONE',  ( 6.838238910409970117, -3.993980678889271552, -6.572970348078615466 ) ) ;
#7143=DIRECTION ( 'NONE',  ( -0.000000000000000000, -0.000000000000000000, 1.000000000000000000 ) ) ;
#7152=CARTESIAN_POINT ( 'NONE',  ( -5.357619327558936585E-16, 7.505553499465137612, -6.064240316920400886 ) ) ;
#7171=CARTESIAN_POINT ( 'NONE',  ( 1.083333333333332593, -6.880090707843051767, -5.848636054922041083 ) ) ;
#7207=ORIENTED_EDGE ( 'NONE', *, *, #2232, .T. ) ;
#7208=ADVANCED_FACE ( 'NONE', ( #7945 ), #8989, .F. ) ;
#7214=DIRECTION ( 'NONE',  ( -1.000000000000000000, 0.000000000000000000, 0.000000000000000000 ) ) ;
#7215=DIRECTION ( 'NONE',  ( 0.000000000000000000, 0.000000000000000000, -1.000000000000000000 ) ) ;
#7240=CARTESIAN_POINT ( 'NONE',  ( 0.000000000000000000, 0.000000000000000000, -8.000000000000000000 ) ) ;
#7243=ORIENTED_EDGE ( 'NONE', *, *, #8996, .F. ) ;
#7247=CARTESIAN_POINT ( 'NONE',  ( -5.450967621166011412, 4.358435876041001578, -0.3607371497494529233 ) ) ;
#7270=ORIENTED_EDGE ( 'NONE', *, *, #3435, .F. ) ;
#7291=CARTESIAN_POINT ( 'NONE',  ( -1.948734328186081425E-15, 7.693909156114108860, -6.460786012260014921 ) ) ;
#7293=AXIS2_PLACEMENT_3D ( 'NONE', #5401, #13296, #11077 ) ;
#7301=CARTESIAN_POINT ( 'NONE',  ( 4.366061277241453098, -4.984806845751389659, -0.09463688534107157768 ) ) ;
#7319=EDGE_CURVE ( 'NONE', #11016, #8855, #13193, .T. ) ;
#7320=PLANE ( 'NONE',  #7773 ) ;
#7332=CARTESIAN_POINT ( 'NONE',  ( -6.837824896291515131, -3.947820044545435447, -6.564402953523717166 ) ) ;
#7356=CARTESIAN_POINT ( 'NONE',  ( 2.971071886220372438, 5.790204346174072647, 1.063026348804146728E-15 ) ) ;
#7365=EDGE_CURVE ( 'NONE', #4582, #11448, #10996, .T. ) ;
#7408=CARTESIAN_POINT ( 'NONE',  ( 5.727634848076855967, 4.575561887447700649, -6.326622577870477215 ) ) ;
#7425=CARTESIAN_POINT ( 'NONE',  ( 6.826575449902429149, 2.663085462279306981, -6.347418139105299950 ) ) ;
#7428=ORIENTED_EDGE ( 'NONE', *, *, #13517, .F. ) ;
#7433=CARTESIAN_POINT ( 'NONE',  ( -6.539196172010139030, 3.775406670193821146, -6.286444963328671420 ) ) ;
#7437=FACE_OUTER_BOUND ( 'NONE', #5335, .T. ) ;
#7444=ORIENTED_EDGE ( 'NONE', *, *, #11652, .T. ) ;
#7478=ORIENTED_EDGE ( 'NONE', *, *, #2363, .F. ) ;
#7485=VERTEX_POINT ( 'NONE', #13695 ) ;
#7498=AXIS2_PLACEMENT_3D ( 'NONE', #12382, #1089, #10250 ) ;
#7508=DIRECTION ( 'NONE',  ( 0.000000000000000000, 0.000000000000000000, 1.000000000000000000 ) ) ;
#7540=CIRCLE ( 'NONE', #14378, 3.999999999999999112 ) ;
#7546=CARTESIAN_POINT ( 'NONE',  ( -1.269541193505925744E-15, 7.895640089090863789, -6.564402953523717166 ) ) ;
#7592=EDGE_CURVE ( 'NONE', #8855, #11016, #208, .T. ) ;
#7599=CARTESIAN_POINT ( 'NONE',  ( 3.399999999999999911, 0.000000000000000000, -0.4201245229258211977 ) ) ;
#7601=CIRCLE ( 'NONE', #5674, 6.500000000000000888 ) ;
#7629=ORIENTED_EDGE ( 'NONE', *, *, #11574, .T. ) ;
#7634=CARTESIAN_POINT ( 'NONE',  ( -5.699988423468465015, -4.591578518468254266, -6.344710093416085606 ) ) ;
#7642=CARTESIAN_POINT ( 'NONE',  ( 0.000000000000000000, 0.000000000000000000, -8.000000000000000000 ) ) ;
#7667=EDGE_CURVE ( 'NONE', #11448, #8086, #1304, .T. ) ;
#7675=CARTESIAN_POINT ( 'NONE',  ( 1.098735407079012738, -7.248058225758961193, -6.326622577870306685 ) ) ;
#7685=DIRECTION ( 'NONE',  ( 0.000000000000000000, 0.000000000000000000, 1.000000000000000000 ) ) ;
#7689=CARTESIAN_POINT ( 'NONE',  ( -3.809068165403726614, -5.306386968807666804, -4.619717694324952472E-15 ) ) ;
#7723=EDGE_CURVE ( 'NONE', #4487, #2113, #6600, .T. ) ;
#7737=ORIENTED_EDGE ( 'NONE', *, *, #5349, .F. ) ;
#7747=CARTESIAN_POINT ( 'NONE',  ( 0.8808064505786590281, 6.997019658119588925, -5.875704392892181716 ) ) ;
#7757=ORIENTED_EDGE ( 'NONE', *, *, #14531, .T. ) ;
#7764=CARTESIAN_POINT ( 'NONE',  ( 6.500000000000000000, -2.501851166488383349, -5.848636054922036642 ) ) ;
#7773=AXIS2_PLACEMENT_3D ( 'NONE', #5267, #2820, #11821 ) ;
#7828=CARTESIAN_POINT ( 'NONE',  ( -3.755786496842903988E-16, -7.505553499465146494, -8.000000000000000000 ) ) ;
#7833=CARTESIAN_POINT ( 'NONE',  ( -5.589124336235484769, -4.278671059406953248, -6.219623095964403880 ) ) ;
#7836=CARTESIAN_POINT ( 'NONE',  ( 6.837824896291514243, 3.947820044545427454, -6.564402953523716278 ) ) ;
#7841=DIRECTION ( 'NONE',  ( 1.000000000000000000, 0.000000000000000000, 0.000000000000000000 ) ) ;
#7874=ORIENTED_EDGE ( 'NONE', *, *, #6899, .T. ) ;
#7902=CARTESIAN_POINT ( 'NONE',  ( 6.539198257602124364, 3.775407874310915179, -6.286450516131049326 ) ) ;
#7909=ADVANCED_FACE ( 'NONE', ( #3569 ), #1192, .F. ) ;
#7932=DIRECTION ( 'NONE',  ( -0.000000000000000000, -0.000000000000000000, 1.000000000000000000 ) ) ;
#7945=FACE_OUTER_BOUND ( 'NONE', #4481, .T. ) ;
#7949=CARTESIAN_POINT ( 'NONE',  ( 4.444974277458119793, -4.939246403833736032, -5.720331885005374595 ) ) ;
#7951=DIRECTION ( 'NONE',  ( 1.000000000000000000, 0.000000000000000000, 0.000000000000000000 ) ) ;
#7962=FACE_OUTER_BOUND ( 'NONE', #11350, .T. ) ;
#7984=AXIS2_PLACEMENT_3D ( 'NONE', #9508, #12544, #4736 ) ;
#7993=CIRCLE ( 'NONE', #6347, 3.399999999999999911 ) ;
#8004=CARTESIAN_POINT ( 'NONE',  ( 6.499999999999999112, -3.752776749732576356, -0.8000000000000003775 ) ) ;
#8011=CARTESIAN_POINT ( 'NONE',  ( 3.999999999999999112, 4.898587196589411843E-16, -7.974599999999998801 ) ) ;
#8020=ADVANCED_FACE ( 'NONE', ( #1555 ), #11662, .F. ) ;
#8060=DIRECTION ( 'NONE',  ( 0.000000000000000000, 0.000000000000000000, 1.000000000000000000 ) ) ;
#8086=VERTEX_POINT ( 'NONE', #2736 ) ;
#8097=CARTESIAN_POINT ( 'NONE',  ( 4.424031367840750129, -4.951337798339555007, -6.056431503347240231 ) ) ;
#8105=CARTESIAN_POINT ( 'NONE',  ( 0.000000000000000000, 0.000000000000000000, -0.4621369752184044666 ) ) ;
#8107=CARTESIAN_POINT ( 'NONE',  ( 8.451592086771722331E-13, 7.790254909845437226, -6.526045885145573600 ) ) ;
#8109=CARTESIAN_POINT ( 'NONE',  ( -1.098735407079250326, -7.248058225758884809, -6.326622577870279152 ) ) ;
#8110=FACE_OUTER_BOUND ( 'NONE', #13806, .T. ) ;
#8115=CARTESIAN_POINT ( 'NONE',  ( 0.2259792476677715822, 7.636022678937395725, -6.470294263593361350 ) ) ;
#8125=ORIENTED_EDGE ( 'NONE', *, *, #4783, .F. ) ;
#8134=CARTESIAN_POINT ( 'NONE',  ( 0.5620262070071402327, -7.564407249984300918, -6.443844059477449093 ) ) ;
#8138=CARTESIAN_POINT ( 'NONE',  ( -2.263183130831070589, 6.566419505188274996, -6.208110906918258287 ) ) ;
#8168=CARTESIAN_POINT ( 'NONE',  ( -6.815830331203684089, 0.6610623347507950109, -6.171384342982605631 ) ) ;
#8179=CARTESIAN_POINT ( 'NONE',  ( -0.8808064505788995024, 6.997019658119450369, -5.875704392893736916 ) ) ;
#8212=( LENGTH_UNIT ( ) NAMED_UNIT ( * ) SI_UNIT ( .MILLI., .METRE. ) );
#8219=CARTESIAN_POINT ( 'NONE',  ( 8.542937654374687995, 0.000000000000000000, -6.800000000000000711 ) ) ;
#8291=EDGE_CURVE ( 'NONE', #1120, #12176, #13777, .T. ) ;
#8309=DIRECTION ( 'NONE',  ( 0.000000000000000000, 0.000000000000000000, -1.000000000000000000 ) ) ;
#8333=CARTESIAN_POINT ( 'NONE',  ( 6.746887896522321348, -3.895317543249584347, -6.526184258131189075 ) ) ;
#8343=CARTESIAN_POINT ( 'NONE',  ( 6.500000000000000888, 0.000000000000000000, 0.000000000000000000 ) ) ;
#8352=EDGE_CURVE ( 'NONE', #2860, #5297, #10787, .T. ) ;
#8357=AXIS2_PLACEMENT_3D ( 'NONE', #10103, #4732, #10028 ) ;
#8369=ADVANCED_FACE ( 'NONE', ( #4515, #4655 ), #2357, .F. ) ;
#8370=B_SPLINE_CURVE_WITH_KNOTS ( 'NONE', 3,
 ( #12367, #3303, #2252, #5799, #10380, #10300, #13407, #9057 ),
 .UNSPECIFIED., .F., .F.,
 ( 4, 2, 2, 4 ),
 ( 2.459764730912720885E-07, 0.001920659145285728234, 0.002880865729692047052, 0.003841072314098365435 ),
 .UNSPECIFIED. ) ;
#8374=PRODUCT_DEFINITION ( 'UNKNOWN', '', #6887, #4288 ) ;
#8376=CARTESIAN_POINT ( 'NONE',  ( 6.500000000000000000, 3.752776749732563921, -6.064240316920399110 ) ) ;
#8393=CARTESIAN_POINT ( 'NONE',  ( -1.101549646961929599E-15, 7.550813340387652950, -6.286444963328673197 ) ) ;
#8401=CARTESIAN_POINT ( 'NONE',  ( 4.639619758716984954, -4.826867782832383824, -0.1499059597315342829 ) ) ;
#8410=CARTESIAN_POINT ( 'NONE',  ( 5.416666666666667851, -4.378239541354669306, -5.848636054922037530 ) ) ;
#8420=EDGE_CURVE ( 'NONE', #7485, #1897, #10034, .T. ) ;
#8425=FACE_OUTER_BOUND ( 'NONE', #12052, .T. ) ;
#8428=DIRECTION ( 'NONE',  ( -0.000000000000000000, -0.000000000000000000, 1.000000000000000000 ) ) ;
#8429=CARTESIAN_POINT ( 'NONE',  ( -3.983107665916332252, 5.570601890521282407, -6.171481112545251335 ) ) ;
#8432=ORIENTED_EDGE ( 'NONE', *, *, #5130, .T. ) ;
#8438=DIRECTION ( 'NONE',  ( 0.000000000000000000, 0.000000000000000000, 1.000000000000000000 ) ) ;
#8469=CARTESIAN_POINT ( 'NONE',  ( 6.500000000000000888, 0.000000000000000000, 0.000000000000000000 ) ) ;
#8476=ORIENTED_EDGE ( 'NONE', *, *, #14531, .F. ) ;
#8510=CARTESIAN_POINT ( 'NONE',  ( -0.2259792476677698891, 7.636022678937394836, -6.470294263593361350 ) ) ;
#8544=CARTESIAN_POINT ( 'NONE',  ( -6.500000000000006217, 3.752776749732561257, -6.177802698399960768 ) ) ;
#8557=CARTESIAN_POINT ( 'NONE',  ( -6.499999999999999112, 1.286902272306389428, -0.09436334093186068972 ) ) ;
#8588=CARTESIAN_POINT ( 'NONE',  ( -2.832728918602883006, -6.234773369952733901, -6.171481112545254000 ) ) ;
#8597=ORIENTED_EDGE ( 'NONE', *, *, #12372, .T. ) ;
#8599=ORIENTED_EDGE ( 'NONE', *, *, #7319, .T. ) ;
#8601=CARTESIAN_POINT ( 'NONE',  ( 6.832273232158034837, 3.329759989367264694, -6.449140625371624580 ) ) ;
#8610=ORIENTED_EDGE ( 'NONE', *, *, #4321, .T. ) ;
#8612=EDGE_CURVE ( 'NONE', #358, #11016, #8832, .T. ) ;
#8623=CARTESIAN_POINT ( 'NONE',  ( -6.500000000000000000, 1.602771114417265164, -0.1495523863686162858 ) ) ;
#8627=CARTESIAN_POINT ( 'NONE',  ( 6.837824896291514243, -3.947820044545437224, -6.564402953523717166 ) ) ;
#8650=CARTESIAN_POINT ( 'NONE',  ( -6.500000000000000888, 4.012863338656273982, -6.470131626772281486 ) ) ;
#8671=CARTESIAN_POINT ( 'NONE',  ( 6.500000000000000888, 1.333904739168207065, -6.094327662196326933 ) ) ;
#8683=ORIENTED_EDGE ( 'NONE', *, *, #10805, .F. ) ;
#8687=( GEOMETRIC_REPRESENTATION_CONTEXT ( 3 ) GLOBAL_UNCERTAINTY_ASSIGNED_CONTEXT ( ( #12557 ) ) GLOBAL_UNIT_ASSIGNED_CONTEXT ( ( #8212, #10580, #1650 ) ) REPRESENTATION_CONTEXT ( 'NONE', 'WORKASPACE' ) );
#8712=CARTESIAN_POINT ( 'NONE',  ( 3.250000000000003109, -5.629165124598849879, 0.000000000000000000 ) ) ;
#8723=CARTESIAN_POINT ( 'NONE',  ( -5.416666666666667851, -4.378239541354669306, -5.848636054922036642 ) ) ;
#8730=CARTESIAN_POINT ( 'NONE',  ( -6.815701034932152069, -1.328907527188669668, -6.169383458210047522 ) ) ;
#8732=AXIS2_PLACEMENT_3D ( 'NONE', #10971, #8977, #5362 ) ;
#8754=CARTESIAN_POINT ( 'NONE',  ( 6.500000000000301981, 0.6542365398607151716, -6.055391205186719361 ) ) ;
#8797=VERTEX_POINT ( 'NONE', #8004 ) ;
#8799=CARTESIAN_POINT ( 'NONE',  ( -4.358513833876417998, -4.989164364209884184, -0.07763482564821273801 ) ) ;
#8802=CARTESIAN_POINT ( 'NONE',  ( 1.127757440534757238, 7.231345287187090243, -6.344532336093706704 ) ) ;
#8804=CARTESIAN_POINT ( 'NONE',  ( -6.815962252199548210, 1.383413844627830791, -6.173425845474762141 ) ) ;
#8811=ORIENTED_EDGE ( 'NONE', *, *, #13505, .T. ) ;
#8828=EDGE_CURVE ( 'NONE', #151, #12920, #9460, .T. ) ;
#8832=LINE ( 'NONE', #3001, #13704 ) ;
#8844=ORIENTED_EDGE ( 'NONE', *, *, #1769, .T. ) ;
#8851=CARTESIAN_POINT ( 'NONE',  ( 2.241046694639346804, 6.576374040526301812, -6.171384342982712212 ) ) ;
#8853=CARTESIAN_POINT ( 'NONE',  ( -6.831979103402614051, -3.295157223185839701, -6.443785395948805395 ) ) ;
#8855=VERTEX_POINT ( 'NONE', #8219 ) ;
#8913=AXIS2_PLACEMENT_3D ( 'NONE', #10764, #510, #4955 ) ;
#8921=CARTESIAN_POINT ( 'NONE',  ( -0.2813450144774468642, 7.667988119308851047, -6.122077150241852728 ) ) ;
#8945=( NAMED_UNIT ( * ) SI_UNIT ( $, .STERADIAN. ) SOLID_ANGLE_UNIT ( ) );
#8969=VECTOR ( 'NONE', #7685, 1000.000000000000000 ) ;
#8970=DIRECTION ( 'NONE',  ( 1.000000000000000000, 0.000000000000000000, 0.000000000000000000 ) ) ;
#8977=DIRECTION ( 'NONE',  ( 0.000000000000000000, 0.000000000000000000, -1.000000000000000000 ) ) ;
#8985=AXIS2_PLACEMENT_3D ( 'NONE', #6030, #3682, #7215 ) ;
#8989=CYLINDRICAL_SURFACE ( 'NONE', #14605, 4.000000000000000000 ) ;
#8995=FACE_OUTER_BOUND ( 'NONE', #5022, .T. ) ;
#8996=EDGE_CURVE ( 'NONE', #2224, #1897, #5927, .T. ) ;
#9019=CARTESIAN_POINT ( 'NONE',  ( 6.837824896291514243, 3.947820044545427454, -6.564402953523716278 ) ) ;
#9021=FACE_OUTER_BOUND ( 'NONE', #3360, .T. ) ;
#9039=CARTESIAN_POINT ( 'NONE',  ( 6.500000000000000000, 3.752776749732563921, -6.064240316920399110 ) ) ;
#9055=CARTESIAN_POINT ( 'NONE',  ( 0.000000000000000000, 0.000000000000000000, 0.000000000000000000 ) ) ;
#9057=CARTESIAN_POINT ( 'NONE',  ( -3.250000000000003997, -5.629165124598849879, 0.000000000000000000 ) ) ;
#9072=PLANE ( 'NONE',  #4176 ) ;
#9092=CARTESIAN_POINT ( 'NONE',  ( -3.755786496842903988E-16, -7.505553499465146494, -6.064240316920404439 ) ) ;
#9093=SURFACE_SIDE_STYLE ('',( #13592 ) ) ;
#9100=ORIENTED_EDGE ( 'NONE', *, *, #7365, .F. ) ;
#9110=ORIENTED_EDGE ( 'NONE', *, *, #2541, .F. ) ;
#9112=DIRECTION ( 'NONE',  ( 1.000000000000000000, 0.000000000000000000, 0.000000000000000000 ) ) ;
#9117=LINE ( 'NONE', #8011, #3004 ) ;
#9119=FACE_OUTER_BOUND ( 'NONE', #10866, .T. ) ;
#9127=ORIENTED_EDGE ( 'NONE', *, *, #3062, .T. ) ;
#9136=DIRECTION ( 'NONE',  ( 1.000000000000000000, 0.000000000000000000, 0.000000000000000000 ) ) ;
#9173=DIRECTION ( 'NONE',  ( -0.000000000000000000, -0.000000000000000000, 1.000000000000000000 ) ) ;
#9222=DIRECTION ( 'NONE',  ( 0.8660254037844382635, 0.5000000000000004441, 0.000000000000000000 ) ) ;
#9242=CARTESIAN_POINT ( 'NONE',  ( -6.815830331203685866, -1.210827632163352847E-13, -6.171384342982610960 ) ) ;
#9247=DIRECTION ( 'NONE',  ( 0.000000000000000000, 0.000000000000000000, 1.000000000000000000 ) ) ;
#9250=CARTESIAN_POINT ( 'NONE',  ( 6.831985876597697072, -3.295913427296349951, -6.443925148804115821 ) ) ;
#9253=CARTESIAN_POINT ( 'NONE',  ( -5.979512004945809700, 4.053280633787070819, -0.5609245978742248839 ) ) ;
#9259=CARTESIAN_POINT ( 'NONE',  ( 3.783380760145018981E-16, -7.895640089090872671, -6.564402953523720718 ) ) ;
#9281=DIRECTION ( 'NONE',  ( -1.000000000000000000, 0.000000000000000000, 0.000000000000000000 ) ) ;
#9293=CARTESIAN_POINT ( 'NONE',  ( -6.500000000000000888, -2.534234941938113828, -0.3584823952106175882 ) ) ;
#9331=DIRECTION ( 'NONE',  ( 1.000000000000000000, 0.000000000000000000, 0.000000000000000000 ) ) ;
#9333=APPLICATION_CONTEXT ( 'automotive_design' ) ;
#9342=DIRECTION ( 'NONE',  ( 0.8191520442889923537, 0.000000000000000000, 0.5735764363510453823 ) ) ;
#9347=FACE_OUTER_BOUND ( 'NONE', #14540, .T. ) ;
#9364=CARTESIAN_POINT ( 'NONE',  ( 6.500000000000000000, 3.752776749732573247, -0.8000000000000003775 ) ) ;
#9390=ORIENTED_EDGE ( 'NONE', *, *, #3455, .T. ) ;
#9394=CARTESIAN_POINT ( 'NONE',  ( -3.811597179862308060, 5.304926841629211687, -0.01956314070068241109 ) ) ;
#9397=CIRCLE ( 'NONE', #1840, 4.000000000000000000 ) ;
#9406=ORIENTED_EDGE ( 'NONE', *, *, #8352, .T. ) ;
#9419=CARTESIAN_POINT ( 'NONE',  ( -8.542937654374687995, 1.046208125374536008E-15, -6.800000000000000711 ) ) ;
#9428=CONICAL_SURFACE ( 'NONE', #3064, 6.500000000000000888, 0.8987552595851582282 ) ;
#9431=CARTESIAN_POINT ( 'NONE',  ( 6.826399921716642005, 2.638123634694624631, -6.344399053232583796 ) ) ;
#9440=AXIS2_PLACEMENT_3D ( 'NONE', #4347, #14302, #6417 ) ;
#9456=CARTESIAN_POINT ( 'NONE',  ( 6.500000000000000000, 3.752776749732563921, -8.000000000000000000 ) ) ;
#9460=CIRCLE ( 'NONE', #12753, 6.500000000000000888 ) ;
#9492=ORIENTED_EDGE ( 'NONE', *, *, #664, .F. ) ;
#9508=CARTESIAN_POINT ( 'NONE',  ( 0.000000000000000000, 0.000000000000000000, -7.381345277524544279 ) ) ;
#9529=B_SPLINE_CURVE_WITH_KNOTS ( 'NONE', 3,
 ( #8469, #11786, #12834, #4873, #11707, #10693, #2715, #5025, #4061, #9364 ),
 .UNSPECIFIED., .F., .F.,
 ( 4, 2, 2, 2, 4 ),
 ( 0.009353627468483380336, 0.01031000219096067476, 0.01126637691343796918, 0.01222275163591526534, 0.01317912635839255976 ),
 .UNSPECIFIED. ) ;
#9557=CARTESIAN_POINT ( 'NONE',  ( -6.270061300899934409, 4.268872906156499170, -6.443866470201760954 ) ) ;
#9574=EDGE_CURVE ( 'NONE', #151, #931, #3423, .T. ) ;
#9575=CARTESIAN_POINT ( 'NONE',  ( 1.860380241283018377, 6.431462466365323927, -0.1499059597315287040 ) ) ;
#9580=CARTESIAN_POINT ( 'NONE',  ( -6.746558653881629120, 3.895127454924392385, -6.526045885145571823 ) ) ;
#9582=VERTEX_POINT ( 'NONE', #1848 ) ;
#9590=ORIENTED_EDGE ( 'NONE', *, *, #5893, .T. ) ;
#9605=CONICAL_SURFACE ( 'NONE', #6543, 6.500000000000000888, 0.8987552595851582282 ) ;
#9618=CARTESIAN_POINT ( 'NONE',  ( 6.781345014477444977, 3.590342129888852263, -6.122077150241850951 ) ) ;
#9656=DIRECTION ( 'NONE',  ( 0.000000000000000000, 0.000000000000000000, -1.000000000000000000 ) ) ;
#9660=DIRECTION ( 'NONE',  ( -1.000000000000000000, 1.224646799147354686E-16, 0.000000000000000000 ) ) ;
#9661=AXIS2_PLACEMENT_3D ( 'NONE', #1372, #11268, #5877 ) ;
#9674=LINE ( 'NONE', #12016, #951 ) ;
#9680=DIRECTION ( 'NONE',  ( -0.000000000000000000, -0.000000000000000000, -1.000000000000000000 ) ) ;
#9698=ORIENTED_EDGE ( 'NONE', *, *, #8828, .T. ) ;
#9701=CARTESIAN_POINT ( 'NONE',  ( 4.574783636564339950, 5.228990388887490681, -6.171384342982508819 ) ) ;
#9707=CONICAL_SURFACE ( 'NONE', #3341, 6.500000000000000888, 0.8987552595851582282 ) ;
#9712=DIRECTION ( 'NONE',  ( 1.000000000000000000, 0.000000000000000000, 0.000000000000000000 ) ) ;
#9713=EDGE_CURVE ( 'NONE', #13126, #2860, #391, .T. ) ;
#9738=DIRECTION ( 'NONE',  ( -0.8191520442889917986, 0.000000000000000000, -0.5735764363510460484 ) ) ;
#9749=CARTESIAN_POINT ( 'NONE',  ( -4.411504479843656235E-13, -7.790635086498889805, -6.526184258131195293 ) ) ;
#9759=B_SPLINE_CURVE_WITH_KNOTS ( 'NONE', 3,
 ( #14265, #7764, #1998, #12038, #12252 ),
 .UNSPECIFIED., .F., .F.,
 ( 4, 1, 4 ),
 ( 0.000000000000000000, 0.003752776749732568765, 0.007505553499465137529 ),
 .UNSPECIFIED. ) ;
#9771=ORIENTED_EDGE ( 'NONE', *, *, #6217, .F. ) ;
#9775=CARTESIAN_POINT ( 'NONE',  ( -3.999999999999999112, 0.000000000000000000, -7.974599999999998801 ) ) ;
#9816=CARTESIAN_POINT ( 'NONE',  ( -6.815830331203685866, -0.6619522098568484392, -6.171384342982615401 ) ) ;
#9822=ADVANCED_FACE ( 'NONE', ( #4956 ), #13378, .F. ) ;
#9861=ORIENTED_EDGE ( 'NONE', *, *, #4054, .T. ) ;
#9863=CARTESIAN_POINT ( 'NONE',  ( -6.500000000000000000, 3.752776749732564809, -0.7999999999999969358 ) ) ;
#9877=CARTESIAN_POINT ( 'NONE',  ( -0.04050535873993951069, -7.919512791578242172, -6.573129608219095310 ) ) ;
#9898=CARTESIAN_POINT ( 'NONE',  ( -3.250000000000003997, -5.629165124598849879, 0.000000000000000000 ) ) ;
#9906=EDGE_CURVE ( 'NONE', #11133, #1120, #9759, .T. ) ;
#9908=EDGE_LOOP ( 'NONE', ( #1631, #14498, #11332, #315, #4426 ) ) ;
#9909=CONICAL_SURFACE ( 'NONE', #8732, 6.500000000000000888, 0.8987552595851582282 ) ;
#9948=STYLED_ITEM ( 'NONE', ( #10047 ), #4558 ) ;
#9953=CONICAL_SURFACE ( 'NONE', #1468, 3.339999999999998970, 0.9599310885968821427 ) ;
#9965=CARTESIAN_POINT ( 'NONE',  ( 4.444974277457895973, 4.939246403833855936, -5.720331885005371042 ) ) ;
#9972=CARTESIAN_POINT ( 'NONE',  ( -6.500000000000000000, 2.501851166488374911, -5.848636054922034866 ) ) ;
#9978=CARTESIAN_POINT ( 'NONE',  ( 2.832728918602883006, 6.234773369952725020, -6.171481112545252223 ) ) ;
#9982=EDGE_CURVE ( 'NONE', #3582, #12176, #3774, .T. ) ;
#9983=ORIENTED_EDGE ( 'NONE', *, *, #5250, .F. ) ;
#10028=DIRECTION ( 'NONE',  ( -1.000000000000000000, 0.000000000000000000, 0.000000000000000000 ) ) ;
#10029=ORIENTED_EDGE ( 'NONE', *, *, #12749, .T. ) ;
#10034=LINE ( 'NONE', #3248, #8969 ) ;
#10041=CARTESIAN_POINT ( 'NONE',  ( -2.075968632161309557, 6.306992450857741517, -6.056431503346038525 ) ) ;
#10047=PRESENTATION_STYLE_ASSIGNMENT (( #11229 ) ) ;
#10091=DIRECTION ( 'NONE',  ( -0.000000000000000000, -0.000000000000000000, 1.000000000000000000 ) ) ;
#10096=DIRECTION ( 'NONE',  ( 1.000000000000000000, 0.000000000000000000, 0.000000000000000000 ) ) ;
#10098=CONICAL_SURFACE ( 'NONE', #7498, 3.339999999999998970, 0.9599310885968821427 ) ;
#10103=CARTESIAN_POINT ( 'NONE',  ( 0.000000000000000000, 0.000000000000000000, 0.000000000000000000 ) ) ;
#10130=ORIENTED_EDGE ( 'NONE', *, *, #1586, .T. ) ;
#10136=TOROIDAL_SURFACE ( 'NONE', #6142, 8.331345277524542681, 0.6186547224754559426 ) ;
#10186=FACE_OUTER_BOUND ( 'NONE', #2685, .T. ) ;
#10197=CARTESIAN_POINT ( 'NONE',  ( -3.249999999999996891, 5.629165124598855208, -5.592027715088710771 ) ) ;
#10250=DIRECTION ( 'NONE',  ( 1.000000000000000000, 0.000000000000000000, 0.000000000000000000 ) ) ;
#10252=ORIENTED_EDGE ( 'NONE', *, *, #6024, .T. ) ;
#10265=CARTESIAN_POINT ( 'NONE',  ( -6.746558653883096390, -3.895127454921857524, -6.526045885145573600 ) ) ;
#10273=FILL_AREA_STYLE ('',( #975 ) ) ;
#10276=ORIENTED_EDGE ( 'NONE', *, *, #9982, .T. ) ;
#10284=CARTESIAN_POINT ( 'NONE',  ( -1.604619215278546562E-14, -7.505553499465138501, -0.8000000000000003775 ) ) ;
#10300=CARTESIAN_POINT ( 'NONE',  ( -2.688402820137703930, -5.953403407568491623, -0.01956314070068837160 ) ) ;
#10311=CARTESIAN_POINT ( 'NONE',  ( 5.727634848075544127, -4.575561887445499742, -6.326622577869666308 ) ) ;
#10317=CARTESIAN_POINT ( 'NONE',  ( 6.500000000000000000, 3.752776749732563921, -8.000000000000000000 ) ) ;
#10320=ORIENTED_EDGE ( 'NONE', *, *, #4263, .T. ) ;
#10321=CARTESIAN_POINT ( 'NONE',  ( 0.000000000000000000, 0.000000000000000000, 0.000000000000000000 ) ) ;
#10359=VECTOR ( 'NONE', #1483, 1000.000000000000000 ) ;
#10380=CARTESIAN_POINT ( 'NONE',  ( -2.133938722758560669, -6.273523403446323421, -0.09463688534107154993 ) ) ;
#10400=FACE_OUTER_BOUND ( 'NONE', #3206, .T. ) ;
#10426=ORIENTED_EDGE ( 'NONE', *, *, #7723, .T. ) ;
#10455=LINE ( 'NONE', #4850, #4184 ) ;
#10456=ORIENTED_EDGE ( 'NONE', *, *, #11956, .F. ) ;
#10464=ORIENTED_EDGE ( 'NONE', *, *, #9906, .T. ) ;
#10472=PLANE ( 'NONE',  #13017 ) ;
#10501=CARTESIAN_POINT ( 'NONE',  ( 6.837824896291514243, -3.947820044545437224, -6.564402953523717166 ) ) ;
#10503=DIRECTION ( 'NONE',  ( 0.000000000000000000, 0.000000000000000000, 1.000000000000000000 ) ) ;
#10525=VERTEX_POINT ( 'NONE', #1382 ) ;
#10531=ORIENTED_EDGE ( 'NONE', *, *, #4951, .T. ) ;
#10534=AXIS2_PLACEMENT_3D ( 'NONE', #3027, #5320, #5174 ) ;
#10551=CARTESIAN_POINT ( 'NONE',  ( -6.663120783604507658, -3.846954578057057983, -6.460786012260014033 ) ) ;
#10567=CARTESIAN_POINT ( 'NONE',  ( 0.000000000000000000, 0.000000000000000000, 0.000000000000000000 ) ) ;
#10580=( NAMED_UNIT ( * ) PLANE_ANGLE_UNIT ( ) SI_UNIT ( $, .RADIAN. ) );
#10610=CARTESIAN_POINT ( 'NONE',  ( 0.000000000000000000, 0.000000000000000000, 0.000000000000000000 ) ) ;
#10614=EDGE_LOOP ( 'NONE', ( #12452, #4164, #2626, #3288, #2649 ) ) ;
#10626=EDGE_CURVE ( 'NONE', #12254, #12397, #2713, .T. ) ;
#10634=CARTESIAN_POINT ( 'NONE',  ( 5.450967621166010524, -4.358435876041012236, -0.3607371497494579193 ) ) ;
#10646=ORIENTED_EDGE ( 'NONE', *, *, #5349, .T. ) ;
#10673=CARTESIAN_POINT ( 'NONE',  ( 0.000000000000000000, 0.000000000000000000, 0.000000000000000000 ) ) ;
#10678=DIRECTION ( 'NONE',  ( -1.000000000000000000, 0.000000000000000000, 0.000000000000000000 ) ) ;
#10693=CARTESIAN_POINT ( 'NONE',  ( 6.500000000000000000, 2.227636940139130051, -0.2900584647821234374 ) ) ;
#10715=CONICAL_SURFACE ( 'NONE', #8357, 6.500000000000000888, 0.8987552595851582282 ) ;
#10728=ADVANCED_FACE ( 'NONE', ( #11921 ), #4286, .F. ) ;
#10739=CARTESIAN_POINT ( 'NONE',  ( -5.357619327558936585E-16, 7.505553499465137612, -6.064240316920400886 ) ) ;
#10755=DIRECTION ( 'NONE',  ( -0.000000000000000000, -0.000000000000000000, 1.000000000000000000 ) ) ;
#10764=CARTESIAN_POINT ( 'NONE',  ( -5.357619327558936585E-16, 7.505553499465137612, -8.000000000000000000 ) ) ;
#10765=CARTESIAN_POINT ( 'NONE',  ( -3.379472811782913559E-16, -7.505553499465146494, -6.177805531629065428 ) ) ;
#10787=B_SPLINE_CURVE_WITH_KNOTS ( 'NONE', 3,
 ( #5538, #9972, #11369, #3403, #13578 ),
 .UNSPECIFIED., .F., .F.,
 ( 4, 1, 4 ),
 ( 0.000000000000000000, 0.003752776749732568765, 0.007505553499465137529 ),
 .UNSPECIFIED. ) ;
#10791=VECTOR ( 'NONE', #10503, 1000.000000000000000 ) ;
#10797=CARTESIAN_POINT ( 'NONE',  ( -3.978477517404915176, -5.573260695678958321, -6.171287963165198676 ) ) ;
#10805=EDGE_CURVE ( 'NONE', #1897, #11582, #11471, .T. ) ;
#10840=ADVANCED_FACE ( 'NONE', ( #9119 ), #9707, .T. ) ;
#10866=EDGE_LOOP ( 'NONE', ( #5878, #12375, #6247 ) ) ;
#10914=DIRECTION ( 'NONE',  ( 1.224646799147353207E-16, 1.000000000000000000, 0.000000000000000000 ) ) ;
#10921=CARTESIAN_POINT ( 'NONE',  ( -6.500000000000000000, 3.453380256388206782, -0.6809028088495794329 ) ) ;
#10946=CARTESIAN_POINT ( 'NONE',  ( -0.5619217318086660029, -7.564468822943311466, -6.443866470201765395 ) ) ;
#10971=CARTESIAN_POINT ( 'NONE',  ( 0.000000000000000000, 0.000000000000000000, 0.000000000000000000 ) ) ;
#10974=ORIENTED_EDGE ( 'NONE', *, *, #4749, .T. ) ;
#10976=DIRECTION ( 'NONE',  ( 1.000000000000000000, 0.000000000000000000, -0.000000000000000000 ) ) ;
#10982=CARTESIAN_POINT ( 'NONE',  ( -0.2813450144774474748, -7.667988119308860817, -6.122077150241856280 ) ) ;
#10984=CARTESIAN_POINT ( 'NONE',  ( 0.000000000000000000, 0.000000000000000000, -7.974599999999998801 ) ) ;
#10996=B_SPLINE_CURVE_WITH_KNOTS ( 'NONE', 3,
 ( #14151, #3830, #1676, #9575, #3749, #486, #7356, #12747 ),
 .UNSPECIFIED., .F., .F.,
 ( 4, 2, 2, 4 ),
 ( 2.459764730720142121E-07, 0.001920659145285718043, 0.002880865729692040113, 0.003841072314098362400 ),
 .UNSPECIFIED. ) ;
#11007=CARTESIAN_POINT ( 'NONE',  ( 3.783380760145018981E-16, -7.895640089090872671, -6.564402953523720718 ) ) ;
#11013=AXIS2_PLACEMENT_3D ( 'NONE', #13746, #4526, #61 ) ;
#11016=VERTEX_POINT ( 'NONE', #9419 ) ;
#11025=CARTESIAN_POINT ( 'NONE',  ( 6.500000000000000888, 3.402385889607308922, -5.998095356498452269 ) ) ;
#11061=CARTESIAN_POINT ( 'NONE',  ( 4.424031367836657402, 4.951337798342080099, -6.056431503344841261 ) ) ;
#11077=DIRECTION ( 'NONE',  ( 1.000000000000000000, 0.000000000000000000, 0.000000000000000000 ) ) ;
#11083=CARTESIAN_POINT ( 'NONE',  ( -6.500000000000000000, -4.014037567183532218, -6.470355840301004413 ) ) ;
#11091=VERTEX_POINT ( 'NONE', #2927 ) ;
#11133=VERTEX_POINT ( 'NONE', #4327 ) ;
#11136=CARTESIAN_POINT ( 'NONE',  ( 6.500000000000000000, -3.155218591052677990, -0.5622968210053915783 ) ) ;
#11156=CARTESIAN_POINT ( 'NONE',  ( -4.424031367838696660, 4.951337798339958240, -6.056431503346038525 ) ) ;
#11209=CARTESIAN_POINT ( 'NONE',  ( -6.837824896291514243, 3.947820044545427454, -6.564402953523716278 ) ) ;
#11212=CARTESIAN_POINT ( 'NONE',  ( -6.878751942472531411, -3.924677726130930910, -6.573129608219091757 ) ) ;
#11221=EDGE_CURVE ( 'NONE', #12920, #10525, #4702, .T. ) ;
#11229=SURFACE_STYLE_USAGE ( .BOTH. , #9093 ) ;
#11238=EDGE_LOOP ( 'NONE', ( #12042, #8844, #8432, #7444 ) ) ;
#11250=ORIENTED_EDGE ( 'NONE', *, *, #14180, .F. ) ;
#11268=DIRECTION ( 'NONE',  ( -0.000000000000000000, -0.000000000000000000, 1.000000000000000000 ) ) ;
#11273=DIRECTION ( 'NONE',  ( -0.000000000000000000, -0.000000000000000000, 1.000000000000000000 ) ) ;
#11285=CARTESIAN_POINT ( 'NONE',  ( 0.2813450144774466422, -7.667988119308859041, -6.122077150241856280 ) ) ;
#11288=ORIENTED_EDGE ( 'NONE', *, *, #11652, .F. ) ;
#11299=ORIENTED_EDGE ( 'NONE', *, *, #3645, .T. ) ;
#11327=ORIENTED_EDGE ( 'NONE', *, *, #664, .T. ) ;
#11332=ORIENTED_EDGE ( 'NONE', *, *, #4263, .F. ) ;
#11350=EDGE_LOOP ( 'NONE', ( #13850, #823, #12595, #11709 ) ) ;
#11354=ADVANCED_FACE ( 'NONE', ( #8425 ), #1397, .F. ) ;
#11360=CARTESIAN_POINT ( 'NONE',  ( -6.499999999999999112, -1.280811194704858158, -0.07768058122908438889 ) ) ;
#11369=CARTESIAN_POINT ( 'NONE',  ( -6.500000000000001776, -2.602085213965210642E-15, -5.592027715088707218 ) ) ;
#11380=CARTESIAN_POINT ( 'NONE',  ( -0.5219667817988843384, 7.204195837485507958, -0.5602453477493336553 ) ) ;
#11386=CARTESIAN_POINT ( 'NONE',  ( 6.826425371444817536, -2.641426549045776451, -6.344843397090116355 ) ) ;
#11389=CONICAL_SURFACE ( 'NONE', #11849, 3.999999999999999112, 0.9599310885968813656 ) ;
#11425=FACE_OUTER_BOUND ( 'NONE', #4309, .T. ) ;
#11428=CARTESIAN_POINT ( 'NONE',  ( -6.500000000000000888, 0.000000000000000000, 0.000000000000000000 ) ) ;
#11439=CARTESIAN_POINT ( 'NONE',  ( -3.755786496842903988E-16, -7.505553499465146494, -6.064240316920404439 ) ) ;
#11440=B_SPLINE_CURVE_WITH_KNOTS ( 'NONE', 3,
 ( #2936, #14157, #9431, #12972, #3005, #3905 ),
 .UNSPECIFIED., .F., .F.,
 ( 4, 2, 4 ),
 ( 0.000000000000000000, 0.001990940508721409253, 0.003981881017442818506 ),
 .UNSPECIFIED. ) ;
#11445=CARTESIAN_POINT ( 'NONE',  ( 3.250000000000001332, -5.629165124598862313, -5.592027715088713435 ) ) ;
#11448=VERTEX_POINT ( 'NONE', #5599 ) ;
#11449=ORIENTED_EDGE ( 'NONE', *, *, #12749, .F. ) ;
#11457=CARTESIAN_POINT ( 'NONE',  ( 5.698650001973517121, -4.592339236403569558, -6.344532336093708480 ) ) ;
#11462=PRODUCT_DEFINITION_SHAPE ( 'NONE', 'NONE',  #8374 ) ;
#11471=LINE ( 'NONE', #5731, #12996 ) ;
#11483=ADVANCED_FACE ( 'NONE', ( #266 ), #9953, .F. ) ;
#11491=CARTESIAN_POINT ( 'NONE',  ( -6.500000000000000000, -0.6456425506958733962, 7.521652571618187011E-16 ) ) ;
#11496=CARTESIAN_POINT ( 'NONE',  ( -4.574783636564919931, -5.228990388887469365, -6.171384342982607407 ) ) ;
#11558=VECTOR ( 'NONE', #8438, 1000.000000000000000 ) ;
#11574=EDGE_CURVE ( 'NONE', #931, #2113, #13290, .T. ) ;
#11575=EDGE_LOOP ( 'NONE', ( #10456, #9390, #12384, #13429, #3445 ) ) ;
#11582=VERTEX_POINT ( 'NONE', #5812 ) ;
#11584=LINE ( 'NONE', #9456, #10359 ) ;
#11590=ADVANCED_FACE ( 'NONE', ( #10400 ), #10472, .T. ) ;
#11651=CARTESIAN_POINT ( 'NONE',  ( -6.539196172010138142, -3.775406670193829584, -6.286444963328671420 ) ) ;
#11652=EDGE_CURVE ( 'NONE', #6727, #12397, #1234, .T. ) ;
#11656=UNCERTAINTY_MEASURE_WITH_UNIT (LENGTH_MEASURE( 1.000000000000000082E-05 ), #13305, 'distance_accuracy_value', 'NONE');
#11662=CYLINDRICAL_SURFACE ( 'NONE', #2840, 3.399999999999999911 ) ;
#11678=FACE_OUTER_BOUND ( 'NONE', #5641, .T. ) ;
#11707=CARTESIAN_POINT ( 'NONE',  ( 6.500000000000000000, 1.602771114417268050, -0.1495523863686167576 ) ) ;
#11709=ORIENTED_EDGE ( 'NONE', *, *, #3455, .F. ) ;
#11751=TOROIDAL_SURFACE ( 'NONE', #7984, 8.331345277524542681, 0.6186547224754559426 ) ;
#11762=CARTESIAN_POINT ( 'NONE',  ( 6.826581433398040133, -2.695947255479557381, -6.331032031596317999 ) ) ;
#11777=DIRECTION ( 'NONE',  ( 0.000000000000000000, 0.000000000000000000, 1.000000000000000000 ) ) ;
#11778=AXIS2_PLACEMENT_3D ( 'NONE', #6747, #7932, #8970 ) ;
#11786=CARTESIAN_POINT ( 'NONE',  ( 6.500000000000000888, 0.3213925021621134026, 6.640738306473707756E-16 ) ) ;
#11801=CARTESIAN_POINT ( 'NONE',  ( 6.499999999999999112, -3.752776749732576356, -0.8000000000000003775 ) ) ;
#11821=DIRECTION ( 'NONE',  ( 0.8660254037844382635, -0.5000000000000006661, 0.000000000000000000 ) ) ;
#11835=ORIENTED_EDGE ( 'NONE', *, *, #12372, .F. ) ;
#11849=AXIS2_PLACEMENT_3D ( 'NONE', #537, #4989, #7118 ) ;
#11894=CARTESIAN_POINT ( 'NONE',  ( 2.055025722542103583, 6.319083845363847374, -5.720331885005371042 ) ) ;
#11921=FACE_OUTER_BOUND ( 'NONE', #12585, .T. ) ;
#11922=LINE ( 'NONE', #1817, #14139 ) ;
#11927=ORIENTED_EDGE ( 'NONE', *, *, #10805, .T. ) ;
#11934=CIRCLE ( 'NONE', #10534, 3.399999999999999911 ) ;
#11954=FACE_OUTER_BOUND ( 'NONE', #11575, .T. ) ;
#11956=EDGE_CURVE ( 'NONE', #5297, #931, #3671, .T. ) ;
#11958=CIRCLE ( 'NONE', #12189, 8.331345277524542681 ) ;
#12012=ORIENTED_EDGE ( 'NONE', *, *, #3062, .F. ) ;
#12016=CARTESIAN_POINT ( 'NONE',  ( 4.000000000000000000, 0.000000000000000000, -25.03750572909317285 ) ) ;
#12030=EDGE_LOOP ( 'NONE', ( #12440, #9127, #10646, #4373 ) ) ;
#12038=CARTESIAN_POINT ( 'NONE',  ( 6.500000000000002665, 2.501851166488374911, -5.848636054922036642 ) ) ;
#12041=CARTESIAN_POINT ( 'NONE',  ( -6.500000000000000888, 2.759383090082417667, -5.880088986491048608 ) ) ;
#12042=ORIENTED_EDGE ( 'NONE', *, *, #10626, .F. ) ;
#12052=EDGE_LOOP ( 'NONE', ( #5360, #12128, #13893, #7478 ) ) ;
#12053=EDGE_LOOP ( 'NONE', ( #12990, #6749, #5427, #10426, #8610, #9698 ) ) ;
#12128=ORIENTED_EDGE ( 'NONE', *, *, #9982, .F. ) ;
#12157=CARTESIAN_POINT ( 'NONE',  ( 2.055025722541879318, -6.319083845363985930, -5.720331885005374595 ) ) ;
#12172=CARTESIAN_POINT ( 'NONE',  ( -5.978033218201117549, -4.054134411712201569, -0.5602453477493345435 ) ) ;
#12175=CARTESIAN_POINT ( 'NONE',  ( 2.262848203703083261, 6.566616684922145453, -6.208169345099790348 ) ) ;
#12176=VERTEX_POINT ( 'NONE', #5786 ) ;
#12177=CARTESIAN_POINT ( 'NONE',  ( -6.499999999999424460, 2.723853875611551789, -6.224027332484248554 ) ) ;
#12189=AXIS2_PLACEMENT_3D ( 'NONE', #2139, #3337, #7841 ) ;
#12196=LINE ( 'NONE', #2089, #5379 ) ;
#12223=DIRECTION ( 'NONE',  ( 0.000000000000000000, 0.000000000000000000, 1.000000000000000000 ) ) ;
#12228=CARTESIAN_POINT ( 'NONE',  ( 0.000000000000000000, 0.000000000000000000, 0.000000000000000000 ) ) ;
#12252=CARTESIAN_POINT ( 'NONE',  ( 6.500000000000000000, 3.752776749732563921, -6.064240316920399110 ) ) ;
#12254=VERTEX_POINT ( 'NONE', #4692 ) ;
#12261=B_SPLINE_CURVE_WITH_KNOTS ( 'NONE', 3,
 ( #13730, #8107, #7291, #8393, #3843, #7152 ),
 .UNSPECIFIED., .F., .F.,
 ( 4, 2, 4 ),
 ( -4.604908129291797664E-06, 0.0003318387708540428594, 0.0006682824498373774944 ),
 .UNSPECIFIED. ) ;
#12283=ORIENTED_EDGE ( 'NONE', *, *, #11221, .T. ) ;
#12328=CARTESIAN_POINT ( 'NONE',  ( -6.500000000000000000, 3.752776749732564809, -8.000000000000000000 ) ) ;
#12329=B_SPLINE_CURVE_WITH_KNOTS ( 'NONE', 3,
 ( #5084, #9580, #13116, #7433, #8544, #3970 ),
 .UNSPECIFIED., .F., .F.,
 ( 4, 2, 4 ),
 ( -4.604908129294308270E-06, 0.0003318387708540395525, 0.0006682824498373734828 ),
 .UNSPECIFIED. ) ;
#12335=ADVANCED_FACE ( 'NONE', ( #11678 ), #11389, .F. ) ;
#12339=CARTESIAN_POINT ( 'NONE',  ( 0.000000000000000000, 0.000000000000000000, -8.000000000000000000 ) ) ;
#12340=MANIFOLD_SOLID_BREP ( 'EndChamfer', #6212 ) ;
#12349=CARTESIAN_POINT ( 'NONE',  ( 2.141486166123590884, -6.269165884987830673, -0.07763482564821427845 ) ) ;
#12367=CARTESIAN_POINT ( 'NONE',  ( -1.604619215278546562E-14, -7.505553499465138501, -0.8000000000000003775 ) ) ;
#12372=EDGE_CURVE ( 'NONE', #6378, #3582, #3725, .T. ) ;
#12375=ORIENTED_EDGE ( 'NONE', *, *, #5239, .F. ) ;
#12382=CARTESIAN_POINT ( 'NONE',  ( 0.000000000000000000, 0.000000000000000000, -0.4621369752184044666 ) ) ;
#12384=ORIENTED_EDGE ( 'NONE', *, *, #2770, .T. ) ;
#12385=CARTESIAN_POINT ( 'NONE',  ( -5.727634848076946561, -4.575561887448768239, -6.326622577870699260 ) ) ;
#12395=PLANE ( 'NONE',  #11013 ) ;
#12397=VERTEX_POINT ( 'NONE', #9775 ) ;
#12400=( LENGTH_UNIT ( ) NAMED_UNIT ( * ) SI_UNIT ( .MILLI., .METRE. ) );
#12415=ORIENTED_EDGE ( 'NONE', *, *, #9713, .T. ) ;
#12433=DIRECTION ( 'NONE',  ( 0.000000000000000000, 0.000000000000000000, -1.000000000000000000 ) ) ;
#12440=ORIENTED_EDGE ( 'NONE', *, *, #13505, .F. ) ;
#12444=CARTESIAN_POINT ( 'NONE',  ( 4.574783636564889733, -5.228990388888015595, -6.171384342982775273 ) ) ;
#12452=ORIENTED_EDGE ( 'NONE', *, *, #3786, .T. ) ;
#12456=CARTESIAN_POINT ( 'NONE',  ( -6.725979247667767780, -3.622307570260316911, -6.470294263593358686 ) ) ;
#12481=CARTESIAN_POINT ( 'NONE',  ( 6.837824896291514243, -3.947820044545437224, -6.564402953523717166 ) ) ;
#12514=DIRECTION ( 'NONE',  ( 0.8191520442889917986, 1.003171929053524747E-16, -0.5735764363510460484 ) ) ;
#12530=CARTESIAN_POINT ( 'NONE',  ( 5.589124336234546853, -4.278671059401403021, -6.219623095963592974 ) ) ;
#12544=DIRECTION ( 'NONE',  ( -0.000000000000000000, -0.000000000000000000, 1.000000000000000000 ) ) ;
#12557=UNCERTAINTY_MEASURE_WITH_UNIT (LENGTH_MEASURE( 1.000000000000000082E-05 ), #8212, 'distance_accuracy_value', 'NONE');
#12569=VERTEX_POINT ( 'NONE', #9092 ) ;
#12585=EDGE_LOOP ( 'NONE', ( #11327, #13784, #7003, #7428 ) ) ;
#12586=CARTESIAN_POINT ( 'NONE',  ( 0.000000000000000000, 0.000000000000000000, 0.000000000000000000 ) ) ;
#12591=CARTESIAN_POINT ( 'NONE',  ( -8.331345277524542681, 1.033251829022860324E-15, -8.000000000000000000 ) ) ;
#12595=ORIENTED_EDGE ( 'NONE', *, *, #3834, .F. ) ;
#12613=CARTESIAN_POINT ( 'NONE',  ( 0.04050535873993867109, -7.919512791578240396, -6.573129608219095310 ) ) ;
#12620=CARTESIAN_POINT ( 'NONE',  ( 0.04050535873994059316, 7.919512791578233291, -6.573129608219092646 ) ) ;
#12622=CARTESIAN_POINT ( 'NONE',  ( -6.837824896291515131, -3.947820044545435447, -6.564402953523717166 ) ) ;
#12624=CARTESIAN_POINT ( 'NONE',  ( 5.699988423468465015, 4.591578518468247161, -6.344710093416081165 ) ) ;
#12643=CARTESIAN_POINT ( 'NONE',  ( 3.999999999999999112, 4.898587196589411843E-16, -7.974599999999998801 ) ) ;
#12644=CARTESIAN_POINT ( 'NONE',  ( -1.126429428730189031, 7.232124035235028892, -6.344710093416086494 ) ) ;
#12670=CARTESIAN_POINT ( 'NONE',  ( -6.500000000000000000, -3.752776749732572803, -6.064240316920399998 ) ) ;
#12723=CARTESIAN_POINT ( 'NONE',  ( -1.269541193505925744E-15, 7.895640089090863789, -6.564402953523717166 ) ) ;
#12725=CARTESIAN_POINT ( 'NONE',  ( 4.358513833876415333, 4.989164364209877967, -0.07763482564820642362 ) ) ;
#12747=CARTESIAN_POINT ( 'NONE',  ( 3.250000000000004441, 5.629165124598849879, 0.000000000000000000 ) ) ;
#12749=EDGE_CURVE ( 'NONE', #12569, #11133, #14035, .T. ) ;
#12753=AXIS2_PLACEMENT_3D ( 'NONE', #12586, #4625, #9112 ) ;
#12762=ORIENTED_EDGE ( 'NONE', *, *, #1065, .T. ) ;
#12803=CARTESIAN_POINT ( 'NONE',  ( 0.000000000000000000, 0.000000000000000000, -25.03750572909317285 ) ) ;
#12807=DIRECTION ( 'NONE',  ( 1.000000000000000000, 0.000000000000000000, 0.000000000000000000 ) ) ;
#12813=FACE_OUTER_BOUND ( 'NONE', #1593, .T. ) ;
#12815=VERTEX_POINT ( 'NONE', #8343 ) ;
#12818=FACE_OUTER_BOUND ( 'NONE', #4241, .T. ) ;
#12829=ORIENTED_EDGE ( 'NONE', *, *, #6731, .F. ) ;
#12833=CARTESIAN_POINT ( 'NONE',  ( 0.000000000000000000, 0.000000000000000000, -7.974599999999998801 ) ) ;
#12834=CARTESIAN_POINT ( 'NONE',  ( 6.500000000000000000, 0.6470732608156823940, -0.01945970098673075951 ) ) ;
#12846=EDGE_CURVE ( 'NONE', #5143, #8855, #1924, .T. ) ;
#12860=CARTESIAN_POINT ( 'NONE',  ( 0.000000000000000000, 0.000000000000000000, 3.469446951953614189E-15 ) ) ;
#12920=VERTEX_POINT ( 'NONE', #8712 ) ;
#12938=CARTESIAN_POINT ( 'NONE',  ( -0.04050535873993896946, 7.919512791578231514, -6.573129608219091757 ) ) ;
#12952=DIRECTION ( 'NONE',  ( -0.000000000000000000, -0.000000000000000000, 1.000000000000000000 ) ) ;
#12960=CARTESIAN_POINT ( 'NONE',  ( 6.815765296784352500, 0.6502800852031724865, -6.170377922158368555 ) ) ;
#12972=CARTESIAN_POINT ( 'NONE',  ( 6.818272094961329799, 1.321852500971154365, -6.208027553811807486 ) ) ;
#12977=AXIS2_PLACEMENT_3D ( 'NONE', #1735, #12952, #2698 ) ;
#12990=ORIENTED_EDGE ( 'NONE', *, *, #5239, .T. ) ;
#12991=PLANE ( 'NONE',  #8913 ) ;
#12996=VECTOR ( 'NONE', #5658, 999.9999999999998863 ) ;
#13017=AXIS2_PLACEMENT_3D ( 'NONE', #10317, #13507, #5749 ) ;
#13018=CARTESIAN_POINT ( 'NONE',  ( -3.250000000000003997, -5.629165124598849879, 0.000000000000000000 ) ) ;
#13051=B_SPLINE_CURVE_WITH_KNOTS ( 'NONE', 3,
 ( #8376, #548, #5073, #3953, #10739 ),
 .UNSPECIFIED., .F., .F.,
 ( 4, 1, 4 ),
 ( 0.000000000000000000, 0.003752776749732569198, 0.007505553499465138396 ),
 .UNSPECIFIED. ) ;
#13063=CARTESIAN_POINT ( 'NONE',  ( -6.499999999999999112, 2.227636940139124722, -0.2900584647821222717 ) ) ;
#13073=CARTESIAN_POINT ( 'NONE',  ( -6.826399921716642005, -2.638123634694629516, -6.344399053232583796 ) ) ;
#13102=ORIENTED_EDGE ( 'NONE', *, *, #5130, .F. ) ;
#13109=EDGE_LOOP ( 'NONE', ( #8683, #10531, #9590, #3528 ) ) ;
#13116=CARTESIAN_POINT ( 'NONE',  ( -6.663120783604506769, 3.846954578057049545, -6.460786012260013145 ) ) ;
#13119=CARTESIAN_POINT ( 'NONE',  ( 0.000000000000000000, 0.000000000000000000, -7.974599999999998801 ) ) ;
#13125=CARTESIAN_POINT ( 'NONE',  ( -6.500000000000000000, 0.3213925021621126255, 6.556035011748282652E-16 ) ) ;
#13126=VERTEX_POINT ( 'NONE', #13735 ) ;
#13129=ADVANCED_FACE ( 'NONE', ( #8110 ), #11751, .T. ) ;
#13130=CARTESIAN_POINT ( 'NONE',  ( 9.356499856268396542E-16, -7.550815748621849011, -6.286450516131055544 ) ) ;
#13167=DIRECTION ( 'NONE',  ( 0.000000000000000000, 0.000000000000000000, -1.000000000000000000 ) ) ;
#13175=CARTESIAN_POINT ( 'NONE',  ( 6.838249506730350369, 3.995160516047499222, -6.573190279698081895 ) ) ;
#13176=AXIS2_PLACEMENT_3D ( 'NONE', #7642, #7143, #6027 ) ;
#13192=FACE_OUTER_BOUND ( 'NONE', #12053, .T. ) ;
#13193=CIRCLE ( 'NONE', #9661, 8.542937654374687995 ) ;
#13225=CARTESIAN_POINT ( 'NONE',  ( -5.441945782601304238, -4.363644636964928658, -0.3576316571898465746 ) ) ;
#13238=CARTESIAN_POINT ( 'NONE',  ( 3.783380760145018981E-16, -7.895640089090872671, -6.564402953523720718 ) ) ;
#13250=( GEOMETRIC_REPRESENTATION_CONTEXT ( 3 ) GLOBAL_UNCERTAINTY_ASSIGNED_CONTEXT ( ( #4752 ) ) GLOBAL_UNIT_ASSIGNED_CONTEXT ( ( #12400, #6591, #1190 ) ) REPRESENTATION_CONTEXT ( 'NONE', 'WORKASPACE' ) );
#13281=CARTESIAN_POINT ( 'NONE',  ( 0.8808064505790902388, -6.997019658119350005, -5.875704392893848826 ) ) ;
#13290=B_SPLINE_CURVE_WITH_KNOTS ( 'NONE', 3,
 ( #7069, #6991, #9293, #11360, #11491, #5971 ),
 .UNSPECIFIED., .F., .F.,
 ( 4, 2, 4 ),
 ( 0.005511122051665409173, 0.007432374760074394321, 0.009353627468483380336 ),
 .UNSPECIFIED. ) ;
#13296=DIRECTION ( 'NONE',  ( -0.000000000000000000, -0.000000000000000000, -1.000000000000000000 ) ) ;
#13300=CARTESIAN_POINT ( 'NONE',  ( -6.500000000000001776, -2.692912473542373952, -6.218066308278946686 ) ) ;
#13305=( LENGTH_UNIT ( ) NAMED_UNIT ( * ) SI_UNIT ( .MILLI., .METRE. ) );
#13328=DIRECTION ( 'NONE',  ( -0.9396926207859143121, 0.000000000000000000, -0.3420201433256525592 ) ) ;
#13347=CARTESIAN_POINT ( 'NONE',  ( 6.725979247667768668, 3.622307570260308918, -6.470294263593358686 ) ) ;
#13378=( BOUNDED_SURFACE ( )  B_SPLINE_SURFACE ( 3, 2, ( 
 ( #13741, #8115, #12620 ),
 ( #8179, #2580, #7083 ),
 ( #815, #10041, #3256 ),
 ( #2062, #11156, #13444 ),
 ( #4372, #14547, #1101 ),
 ( #5331, #14333, #2144 ) ),
 .UNSPECIFIED., .F., .F., .T. ) 
 B_SPLINE_SURFACE_WITH_KNOTS ( ( 4, 2, 4 ),
 ( 3, 3 ),
 ( 0.003190620565844218184, 0.007281897438794484971, 0.01137317431174475132 ),
 ( 0.000000000000000000, 1.000000000000000000 ),
 .UNSPECIFIED. ) 
 GEOMETRIC_REPRESENTATION_ITEM ( )  RATIONAL_B_SPLINE_SURFACE ( (
 ( 1.000000000000000000, 0.8047731410850399447, 1.000000000000000000),
 ( 1.000000000000000000, 0.8125552299156222347, 1.000000000000000000),
 ( 1.000000000000000000, 0.8191520442889872466, 1.000000000000000000),
 ( 1.000000000000000000, 0.8191520442889872466, 1.000000000000000000),
 ( 1.000000000000000000, 0.8125552299156223457, 1.000000000000000000),
 ( 1.000000000000000000, 0.8047731410850402778, 1.000000000000000000) ) ) 
 REPRESENTATION_ITEM ( '' )  SURFACE ( )  );
#13381=AXIS2_PLACEMENT_3D ( 'NONE', #1587, #9281, #3957 ) ;
#13407=CARTESIAN_POINT ( 'NONE',  ( -2.971071886220377323, -5.790204346174079753, -4.679857033580009373E-15 ) ) ;
#13409=ADVANCED_FACE ( 'NONE', ( #3086, #13192 ), #3009, .T. ) ;
#13429=ORIENTED_EDGE ( 'NONE', *, *, #6217, .T. ) ;
#13444=CARTESIAN_POINT ( 'NONE',  ( -4.574783636564603739, 5.228990388888020036, -6.171384342982724647 ) ) ;
#13467=AXIS2_PLACEMENT_3D ( 'NONE', #13119, #5306, #1974 ) ;
#13505=EDGE_CURVE ( 'NONE', #13769, #11016, #5183, .T. ) ;
#13507=DIRECTION ( 'NONE',  ( 0.5000000000000006661, 0.8660254037844383745, -0.000000000000000000 ) ) ;
#13511=ADVANCED_FACE ( 'NONE', ( #7437 ), #5417, .T. ) ;
#13512=CARTESIAN_POINT ( 'NONE',  ( -2.241046694638765935, -6.576374040526340892, -6.171384342982618065 ) ) ;
#13517=EDGE_CURVE ( 'NONE', #7485, #12397, #11922, .T. ) ;
#13523=CARTESIAN_POINT ( 'NONE',  ( 3.978477517404916064, 5.573260695678954768, -6.171287963165197787 ) ) ;
#13553=ORIENTED_EDGE ( 'NONE', *, *, #12846, .F. ) ;
#13562=ORIENTED_EDGE ( 'NONE', *, *, #2232, .F. ) ;
#13568=CARTESIAN_POINT ( 'NONE',  ( -6.818286579240217193, 1.325012739682870810, -6.208253321455267759 ) ) ;
#13569=DIRECTION ( 'NONE',  ( 0.5000000000000005551, -0.8660254037844383745, 0.000000000000000000 ) ) ;
#13578=CARTESIAN_POINT ( 'NONE',  ( -6.500000000000000000, -3.752776749732572803, -6.064240316920399998 ) ) ;
#13582=CARTESIAN_POINT ( 'NONE',  ( -5.416666666666670515, 4.378239541354659536, -5.848636054922036642 ) ) ;
#13592=SURFACE_STYLE_FILL_AREA ( #10273 ) ;
#13645=CIRCLE ( 'NONE', #4934, 3.999999999999999112 ) ;
#13650=ORIENTED_EDGE ( 'NONE', *, *, #622, .T. ) ;
#13695=CARTESIAN_POINT ( 'NONE',  ( -3.399999999999999911, 4.163799117101000559E-16, -7.554475477074173106 ) ) ;
#13699=AXIS2_PLACEMENT_3D ( 'NONE', #1049, #3273, #1953 ) ;
#13704=VECTOR ( 'NONE', #13328, 1000.000000000000000 ) ;
#13730=CARTESIAN_POINT ( 'NONE',  ( -1.269541193505925744E-15, 7.895640089090863789, -6.564402953523717166 ) ) ;
#13735=CARTESIAN_POINT ( 'NONE',  ( -5.357619327558936585E-16, 7.505553499465137612, -6.064240316920400886 ) ) ;
#13739=ORIENTED_EDGE ( 'NONE', *, *, #10626, .T. ) ;
#13741=CARTESIAN_POINT ( 'NONE',  ( 0.2813450144774485850, 7.667988119308852824, -6.122077150241853616 ) ) ;
#13746=CARTESIAN_POINT ( 'NONE',  ( 6.500000000000000000, 3.752776749732563921, -8.000000000000000000 ) ) ;
#13765=CARTESIAN_POINT ( 'NONE',  ( -4.555432764205793461, 5.242992371775927474, -6.208169345099788572 ) ) ;
#13769=VERTEX_POINT ( 'NONE', #12591 ) ;
#13777=B_SPLINE_CURVE_WITH_KNOTS ( 'NONE', 3,
 ( #2135, #3468, #7902, #2273, #6785, #7836 ),
 .UNSPECIFIED., .F., .F.,
 ( 4, 2, 4 ),
 ( 0.000000000000000000, 0.0003352299596267567321, 0.0006704599192535134642 ),
 .UNSPECIFIED. ) ;
#13784=ORIENTED_EDGE ( 'NONE', *, *, #5830, .T. ) ;
#13786=EDGE_LOOP ( 'NONE', ( #2182, #12415, #11299, #6939, #10130 ) ) ;
#13796=DIRECTION ( 'NONE',  ( -0.000000000000000000, -0.000000000000000000, 1.000000000000000000 ) ) ;
#13800=DIRECTION ( 'NONE',  ( -0.000000000000000000, -0.000000000000000000, 1.000000000000000000 ) ) ;
#13806=EDGE_LOOP ( 'NONE', ( #13913, #8811, #1052, #7737 ) ) ;
#13818=ORIENTED_EDGE ( 'NONE', *, *, #6731, .T. ) ;
#13821=CARTESIAN_POINT ( 'NONE',  ( -3.528928113779633335, 5.468125903023623557, 1.037615360386517718E-15 ) ) ;
#13843=CARTESIAN_POINT ( 'NONE',  ( 6.500000000000000888, -2.759515168581564204, -5.880113447610522570 ) ) ;
#13850=ORIENTED_EDGE ( 'NONE', *, *, #3786, .F. ) ;
#13851=ADVANCED_FACE ( 'NONE', ( #317 ), #260, .F. ) ;
#13891=CIRCLE ( 'NONE', #1383, 6.500000000000000888 ) ;
#13893=ORIENTED_EDGE ( 'NONE', *, *, #859, .T. ) ;
#13899=DIRECTION ( 'NONE',  ( 1.000000000000000000, 0.000000000000000000, 0.000000000000000000 ) ) ;
#13910=CARTESIAN_POINT ( 'NONE',  ( 6.500000000000000000, -3.752776749732574135, -8.000000000000000000 ) ) ;
#13913=ORIENTED_EDGE ( 'NONE', *, *, #2541, .T. ) ;
#13928=ORIENTED_EDGE ( 'NONE', *, *, #9713, .F. ) ;
#13978=ORIENTED_EDGE ( 'NONE', *, *, #2770, .F. ) ;
#13982=CARTESIAN_POINT ( 'NONE',  ( -4.366061277241453098, 4.984806845751379889, -0.09463688534106590167 ) ) ;
#14032=CARTESIAN_POINT ( 'NONE',  ( 6.815830331203685866, 1.228021141713631082E-13, -6.171384342982610960 ) ) ;
#14035=B_SPLINE_CURVE_WITH_KNOTS ( 'NONE', 3,
 ( #438, #7171, #11445, #8410, #1337 ),
 .UNSPECIFIED., .F., .F.,
 ( 4, 1, 4 ),
 ( 5.644705275899819452E-20, 0.003752776749732567464, 0.007505553499465136662 ),
 .UNSPECIFIED. ) ;
#14081=CARTESIAN_POINT ( 'NONE',  ( -4.000000000000000000, 4.898587196589412829E-16, -25.03750572909317285 ) ) ;
#14104=CARTESIAN_POINT ( 'NONE',  ( 0.000000000000000000, 0.000000000000000000, -8.000000000000000000 ) ) ;
#14126=AXIS2_PLACEMENT_3D ( 'NONE', #10567, #448, #1345 ) ;
#14128=VECTOR ( 'NONE', #5177, 1000.000000000000000 ) ;
#14134=CARTESIAN_POINT ( 'NONE',  ( -5.357619327558936585E-16, 7.505553499465137612, -8.000000000000000000 ) ) ;
#14139=VECTOR ( 'NONE', #9738, 1000.000000000000227 ) ;
#14151=CARTESIAN_POINT ( 'NONE',  ( -4.336808689942017736E-16, 7.505553499465137612, -0.8000000000000003775 ) ) ;
#14157=CARTESIAN_POINT ( 'NONE',  ( 6.831979103402612274, 3.295157223185832596, -6.443785395948806283 ) ) ;
#14163=CARTESIAN_POINT ( 'NONE',  ( 0.000000000000000000, 0.000000000000000000, 0.000000000000000000 ) ) ;
#14180=EDGE_CURVE ( 'NONE', #488, #6919, #4637, .T. ) ;
#14195=CARTESIAN_POINT ( 'NONE',  ( -3.250000000000000444, -5.629165124598859649, -5.592027715088708995 ) ) ;
#14196=( GEOMETRIC_REPRESENTATION_CONTEXT ( 3 ) GLOBAL_UNCERTAINTY_ASSIGNED_CONTEXT ( ( #11656 ) ) GLOBAL_UNIT_ASSIGNED_CONTEXT ( ( #13305, #14555, #8945 ) ) REPRESENTATION_CONTEXT ( 'NONE', 'WORKASPACE' ) );
#14201=CARTESIAN_POINT ( 'NONE',  ( 0.9108756637626340691, 6.979659189792313256, -6.219623095964331050 ) ) ;
#14203=VERTEX_POINT ( 'NONE', #6076 ) ;
#14205=CARTESIAN_POINT ( 'NONE',  ( -6.269955739554009533, -4.268932597852945321, -6.443844059477445541 ) ) ;
#14210=ORIENTED_EDGE ( 'NONE', *, *, #1769, .F. ) ;
#14265=CARTESIAN_POINT ( 'NONE',  ( 6.500000000000000000, -3.752776749732574135, -6.064240316920400886 ) ) ;
#14268=CARTESIAN_POINT ( 'NONE',  ( -6.500000000000000888, 4.076783350660894811, -6.121918786669029444 ) ) ;
#14286=CARTESIAN_POINT ( 'NONE',  ( 6.500000000000000888, 2.723353699433710862, -5.896365680526115760 ) ) ;
#14302=DIRECTION ( 'NONE',  ( 0.000000000000000000, 0.000000000000000000, 1.000000000000000000 ) ) ;
#14309=CARTESIAN_POINT ( 'NONE',  ( 9.573736116531104419E-16, -7.693917458112909280, -6.460793508093584769 ) ) ;
#14326=CONICAL_SURFACE ( 'NONE', #875, 8.542937654374687995, 1.221730476396047926 ) ;
#14333=CARTESIAN_POINT ( 'NONE',  ( -6.725979247667768668, 3.622307570260310694, -6.470294263593358686 ) ) ;
#14337=CARTESIAN_POINT ( 'NONE',  ( -6.500000000000000888, -1.360915494584213459, -5.718331000733963165 ) ) ;
#14357=CARTESIAN_POINT ( 'NONE',  ( 6.818262094730843437, 1.323628772216571381, -6.207787212118422104 ) ) ;
#14362=ORIENTED_EDGE ( 'NONE', *, *, #1586, .F. ) ;
#14369=AXIS2_PLACEMENT_3D ( 'NONE', #5154, #10914, #9660 ) ;
#14378=AXIS2_PLACEMENT_3D ( 'NONE', #10984, #11273, #10096 ) ;
#14381=ORIENTED_EDGE ( 'NONE', *, *, #7592, .T. ) ;
#14397=CARTESIAN_POINT ( 'NONE',  ( 8.542937654374687995, 1.046208125374536008E-15, -6.800000000000000711 ) ) ;
#14400=CIRCLE ( 'NONE', #8985, 0.6186547224754559426 ) ;
#14406=EDGE_CURVE ( 'NONE', #358, #6378, #4243, .T. ) ;
#14407=CARTESIAN_POINT ( 'NONE',  ( -1.269541193505925744E-15, 7.895640089090863789, -6.564402953523717166 ) ) ;
#14440=CARTESIAN_POINT ( 'NONE',  ( 6.499999999999999112, 4.014041399406598210, -6.470356572124273953 ) ) ;
#14469=CARTESIAN_POINT ( 'NONE',  ( -6.818272094961329799, -1.321852500971156363, -6.208027553811807486 ) ) ;
#14472=CARTESIAN_POINT ( 'NONE',  ( -3.399999999999999911, 4.163799117101000559E-16, -0.4201245229258211977 ) ) ;
#14475=CARTESIAN_POINT ( 'NONE',  ( -12.99999999999999112, -3.903127820947815962E-15, -8.000000000000000000 ) ) ;
#14480=DIRECTION ( 'NONE',  ( 0.000000000000000000, 0.000000000000000000, 1.000000000000000000 ) ) ;
#14484=CARTESIAN_POINT ( 'NONE',  ( -6.838249472399978046, -3.995156693690920413, -6.573189567101943354 ) ) ;
#14485=EDGE_LOOP ( 'NONE', ( #893, #6310, #12762, #876 ) ) ;
#14498=ORIENTED_EDGE ( 'NONE', *, *, #6024, .F. ) ;
#14499=VERTEX_POINT ( 'NONE', #5600 ) ;
#14531=EDGE_CURVE ( 'NONE', #12815, #8086, #9529, .T. ) ;
#14540=EDGE_LOOP ( 'NONE', ( #13553, #10252, #1945, #7874, #13650, #3512, #8599 ) ) ;
#14547=CARTESIAN_POINT ( 'NONE',  ( -5.589124336234651658, 4.278671059406048194, -6.219623095967983240 ) ) ;
#14555=( NAMED_UNIT ( * ) PLANE_ANGLE_UNIT ( ) SI_UNIT ( $, .RADIAN. ) );
#14593=( BOUNDED_SURFACE ( )  B_SPLINE_SURFACE ( 3, 2, ( 
 ( #14268, #8650, #4307 ),
 ( #12041, #12177, #1939 ),
 ( #817, #5334, #8804 ),
 ( #14337, #4229, #8730 ),
 ( #2066, #13300, #3193 ),
 ( #6585, #11083, #14484 ) ),
 .UNSPECIFIED., .F., .F., .T. ) 
 B_SPLINE_SURFACE_WITH_KNOTS ( ( 4, 2, 4 ),
 ( 3, 3 ),
 ( 0.03172058138205611361, 0.03571597378202086281, 0.03971136618198560508 ),
 ( 0.000000000000000000, 1.000000000000000000 ),
 .UNSPECIFIED. ) 
 GEOMETRIC_REPRESENTATION_ITEM ( )  RATIONAL_B_SPLINE_SURFACE ( (
 ( 1.000000000000000000, 0.8047780791350982454, 1.000000000000000000),
 ( 1.000000000000000000, 0.8123796029720318224, 1.000000000000000000),
 ( 1.000000000000000000, 0.8190681660673523323, 1.000000000000000000),
 ( 1.000000000000000000, 0.8192342536572917444, 1.000000000000000000),
 ( 1.000000000000000000, 0.8126124427164184150, 1.000000000000000000),
 ( 1.000000000000000000, 0.8047712715942066941, 1.000000000000000000) ) ) 
 REPRESENTATION_ITEM ( '' )  SURFACE ( )  );
#14605=AXIS2_PLACEMENT_3D ( 'NONE', #32, #10091, #4570 ) ;
#14607=CARTESIAN_POINT ( 'NONE',  ( 6.500000000000000000, -0.6456425506958747285, 7.487771253728014997E-16 ) ) ;
#14675=COLOUR_RGB('Black',0.12,0.14,0.17);
#14676=FILL_AREA_STYLE_COLOUR('',#14675);
#14677=FILL_AREA_STYLE('',(#14676));
#14678=SURFACE_STYLE_FILL_AREA(#14677);
#14679=SURFACE_SIDE_STYLE('',(#14678));
#14680=SURFACE_STYLE_USAGE(.BOTH.,#14679);
#14681=PRESENTATION_STYLE_ASSIGNMENT((#14680));
ENDSEC;
END-ISO-10303-21;
